ISO-10303-21;
HEADER;
/* Generated by software containing ST-Developer
 * from STEP Tools, Inc. (www.steptools.com) 
 */

FILE_DESCRIPTION(
/* description */ (''),
/* implementation_level */ '2;1');

FILE_NAME(
/* name */ 'Top_Block.step',
/* time_stamp */ '2026-10-19T02:00:06+06:00',
/* author */ (''),
/* organization */ (''),
/* preprocessor_version */ 'ST-DEVELOPER v20.2',
/* originating_system */ 'Autodesk Translation Framework v15.15.0.0',
/* authorisation */ '');

FILE_SCHEMA (('AUTOMOTIVE_DESIGN { 1 0 10303 214 3 1 1 }'));
ENDSEC;

DATA;
#10=MECHANICAL_DESIGN_GEOMETRIC_PRESENTATION_REPRESENTATION('',(#112),#4833);
#55=SPHERICAL_SURFACE('',#2991,1.00000000000001);
#56=SPHERICAL_SURFACE('',#2997,0.999999999999996);
#57=SPHERICAL_SURFACE('',#3003,0.999999999999996);
#58=SPHERICAL_SURFACE('',#3010,0.999999999999996);
#59=B_SPLINE_CURVE_WITH_KNOTS('',3,(#4296,#4297,#4298,#4299,#4300,#4301,
#4302,#4303,#4304,#4305,#4306,#4307),.UNSPECIFIED.,.F.,.F.,(4,2,2,2,2,4),
(0.,0.104126648162078,0.208253296324155,0.41650659264831,0.61629680537715,
0.81608701810599),.UNSPECIFIED.);
#60=B_SPLINE_CURVE_WITH_KNOTS('',3,(#4308,#4309,#4310,#4311,#4312,#4313,
#4314,#4315,#4316,#4317,#4318,#4319,#4320,#4321,#4322,#4323,#4324,#4325,
#4326,#4327,#4328,#4329,#4330,#4331,#4332,#4333,#4334,#4335,#4336,#4337,
#4338,#4339),.UNSPECIFIED.,.F.,.F.,(4,2,2,2,2,2,2,2,2,2,2,2,2,2,2,4),(0.81608701810599,
1.01587723083483,1.21566744356367,1.42392073988783,1.5280473880499,1.63217403621198,
1.73630068437406,1.84042733253614,2.04868062886029,2.24847084158913,2.44826105431797,
2.64805126704681,2.84784147977565,3.05609477609981,3.16022142426189,3.26434807242396),
 .UNSPECIFIED.);
#61=B_SPLINE_CURVE_WITH_KNOTS('',3,(#4343,#4344,#4345,#4346,#4347,#4348,
#4349,#4350,#4351,#4352,#4353,#4354,#4355,#4356,#4357,#4358,#4359,#4360,
#4361,#4362,#4363,#4364,#4365,#4366,#4367,#4368,#4369,#4370,#4371,#4372,
#4373,#4374),.UNSPECIFIED.,.F.,.F.,(4,2,2,2,2,2,2,2,2,2,2,2,2,2,2,4),(0.,
0.104126648162077,0.208253296324155,0.41650659264831,0.616296805377151,
0.816087018105991,1.01587723083483,1.21566744356367,1.42392073988783,1.52804738804991,
1.63217403621198,1.73630068437406,1.84042733253614,2.04868062886029,2.24847084158913,
2.44826105431797),.UNSPECIFIED.);
#62=B_SPLINE_CURVE_WITH_KNOTS('',3,(#4375,#4376,#4377,#4378,#4379,#4380,
#4381,#4382,#4383,#4384,#4385,#4386),.UNSPECIFIED.,.F.,.F.,(4,2,2,2,2,4),
(2.44826105431797,2.64805126704681,2.84784147977565,3.05609477609981,3.16022142426189,
3.26434807242396),.UNSPECIFIED.);
#63=B_SPLINE_CURVE_WITH_KNOTS('',3,(#4408,#4409,#4410,#4411,#4412,#4413,
#4414,#4415,#4416,#4417,#4418,#4419),.UNSPECIFIED.,.F.,.F.,(4,2,2,2,2,4),
(0.,0.104126648162077,0.208253296324155,0.416506592648309,0.61629680537715,
0.816087018105991),.UNSPECIFIED.);
#64=B_SPLINE_CURVE_WITH_KNOTS('',3,(#4420,#4421,#4422,#4423,#4424,#4425,
#4426,#4427,#4428,#4429,#4430,#4431,#4432,#4433,#4434,#4435,#4436,#4437,
#4438,#4439,#4440,#4441,#4442,#4443,#4444,#4445,#4446,#4447,#4448,#4449,
#4450,#4451),.UNSPECIFIED.,.F.,.F.,(4,2,2,2,2,2,2,2,2,2,2,2,2,2,2,4),(0.816087018105991,
1.01587723083483,1.21566744356367,1.42392073988783,1.5280473880499,1.63217403621198,
1.73630068437406,1.84042733253614,2.04868062886029,2.24847084158913,2.44826105431797,
2.64805126704681,2.84784147977565,3.05609477609981,3.16022142426189,3.26434807242396),
 .UNSPECIFIED.);
#65=B_SPLINE_CURVE_WITH_KNOTS('',3,(#4455,#4456,#4457,#4458,#4459,#4460,
#4461,#4462,#4463,#4464,#4465,#4466,#4467,#4468,#4469,#4470,#4471,#4472,
#4473,#4474,#4475,#4476,#4477,#4478,#4479,#4480,#4481,#4482,#4483,#4484,
#4485,#4486),.UNSPECIFIED.,.F.,.F.,(4,2,2,2,2,2,2,2,2,2,2,2,2,2,2,4),(0.,
0.104126648162077,0.208253296324155,0.416506592648309,0.61629680537715,
0.816087018105991,1.01587723083483,1.21566744356367,1.42392073988783,1.5280473880499,
1.63217403621198,1.73630068437406,1.84042733253614,2.04868062886029,2.24847084158913,
2.44826105431797),.UNSPECIFIED.);
#66=B_SPLINE_CURVE_WITH_KNOTS('',3,(#4487,#4488,#4489,#4490,#4491,#4492,
#4493,#4494,#4495,#4496,#4497,#4498),.UNSPECIFIED.,.F.,.F.,(4,2,2,2,2,4),
(2.44826105431797,2.64805126704681,2.84784147977565,3.05609477609981,3.16022142426189,
3.26434807242396),.UNSPECIFIED.);
#90=SHAPE_REPRESENTATION_RELATIONSHIP('SRR','None',#4881,#101);
#101=ADVANCED_BREP_SHAPE_REPRESENTATION('',(#123),#4829);
#112=STYLED_ITEM('',(#4971),#123);
#123=MANIFOLD_SOLID_BREP('Body1',#2694);
#142=FACE_BOUND('',#559,.T.);
#143=FACE_BOUND('',#563,.T.);
#144=FACE_BOUND('',#564,.T.);
#145=FACE_BOUND('',#565,.T.);
#146=FACE_BOUND('',#566,.T.);
#147=FACE_BOUND('',#567,.T.);
#148=FACE_BOUND('',#568,.T.);
#149=FACE_BOUND('',#570,.T.);
#150=FACE_BOUND('',#571,.T.);
#151=FACE_BOUND('',#572,.T.);
#152=FACE_BOUND('',#573,.T.);
#153=FACE_BOUND('',#577,.T.);
#154=FACE_BOUND('',#578,.T.);
#155=FACE_BOUND('',#582,.T.);
#156=FACE_BOUND('',#583,.T.);
#157=FACE_BOUND('',#590,.T.);
#158=FACE_BOUND('',#592,.T.);
#159=FACE_BOUND('',#593,.T.);
#226=PLANE('',#3019);
#227=PLANE('',#3021);
#228=PLANE('',#3022);
#229=PLANE('',#3023);
#230=PLANE('',#3026);
#231=PLANE('',#3027);
#232=PLANE('',#3028);
#233=PLANE('',#3029);
#234=PLANE('',#3030);
#235=PLANE('',#3031);
#236=PLANE('',#3032);
#237=PLANE('',#3033);
#238=PLANE('',#3034);
#239=PLANE('',#3035);
#240=PLANE('',#3036);
#241=PLANE('',#3037);
#242=PLANE('',#3038);
#243=PLANE('',#3039);
#362=FACE_OUTER_BOUND('',#538,.T.);
#363=FACE_OUTER_BOUND('',#539,.T.);
#364=FACE_OUTER_BOUND('',#540,.T.);
#365=FACE_OUTER_BOUND('',#541,.T.);
#366=FACE_OUTER_BOUND('',#542,.T.);
#367=FACE_OUTER_BOUND('',#543,.T.);
#368=FACE_OUTER_BOUND('',#544,.T.);
#369=FACE_OUTER_BOUND('',#545,.T.);
#370=FACE_OUTER_BOUND('',#546,.T.);
#371=FACE_OUTER_BOUND('',#547,.T.);
#372=FACE_OUTER_BOUND('',#548,.T.);
#373=FACE_OUTER_BOUND('',#549,.T.);
#374=FACE_OUTER_BOUND('',#550,.T.);
#375=FACE_OUTER_BOUND('',#551,.T.);
#376=FACE_OUTER_BOUND('',#552,.T.);
#377=FACE_OUTER_BOUND('',#553,.T.);
#378=FACE_OUTER_BOUND('',#554,.T.);
#379=FACE_OUTER_BOUND('',#555,.T.);
#380=FACE_OUTER_BOUND('',#556,.T.);
#381=FACE_OUTER_BOUND('',#557,.T.);
#382=FACE_OUTER_BOUND('',#558,.T.);
#383=FACE_OUTER_BOUND('',#560,.T.);
#384=FACE_OUTER_BOUND('',#561,.T.);
#385=FACE_OUTER_BOUND('',#562,.T.);
#386=FACE_OUTER_BOUND('',#569,.T.);
#387=FACE_OUTER_BOUND('',#574,.T.);
#388=FACE_OUTER_BOUND('',#575,.T.);
#389=FACE_OUTER_BOUND('',#576,.T.);
#390=FACE_OUTER_BOUND('',#579,.T.);
#391=FACE_OUTER_BOUND('',#580,.T.);
#392=FACE_OUTER_BOUND('',#581,.T.);
#393=FACE_OUTER_BOUND('',#584,.T.);
#394=FACE_OUTER_BOUND('',#585,.T.);
#395=FACE_OUTER_BOUND('',#586,.T.);
#396=FACE_OUTER_BOUND('',#587,.T.);
#397=FACE_OUTER_BOUND('',#588,.T.);
#398=FACE_OUTER_BOUND('',#589,.T.);
#399=FACE_OUTER_BOUND('',#591,.T.);
#400=FACE_OUTER_BOUND('',#594,.T.);
#538=EDGE_LOOP('',(#2147,#2148,#2149,#2150,#2151));
#539=EDGE_LOOP('',(#2152,#2153,#2154,#2155,#2156));
#540=EDGE_LOOP('',(#2157,#2158,#2159,#2160));
#541=EDGE_LOOP('',(#2161,#2162,#2163,#2164));
#542=EDGE_LOOP('',(#2165,#2166,#2167,#2168,#2169));
#543=EDGE_LOOP('',(#2170,#2171,#2172,#2173,#2174));
#544=EDGE_LOOP('',(#2175,#2176,#2177,#2178));
#545=EDGE_LOOP('',(#2179,#2180,#2181,#2182));
#546=EDGE_LOOP('',(#2183,#2184,#2185));
#547=EDGE_LOOP('',(#2186,#2187,#2188,#2189));
#548=EDGE_LOOP('',(#2190,#2191,#2192));
#549=EDGE_LOOP('',(#2193,#2194,#2195,#2196));
#550=EDGE_LOOP('',(#2197,#2198,#2199));
#551=EDGE_LOOP('',(#2200,#2201,#2202,#2203));
#552=EDGE_LOOP('',(#2204,#2205,#2206,#2207));
#553=EDGE_LOOP('',(#2208,#2209,#2210));
#554=EDGE_LOOP('',(#2211,#2212,#2213,#2214));
#555=EDGE_LOOP('',(#2215,#2216,#2217,#2218));
#556=EDGE_LOOP('',(#2219,#2220,#2221,#2222));
#557=EDGE_LOOP('',(#2223,#2224,#2225,#2226));
#558=EDGE_LOOP('',(#2227,#2228,#2229,#2230,#2231,#2232,#2233,#2234,#2235,
#2236,#2237,#2238,#2239,#2240,#2241,#2242));
#559=EDGE_LOOP('',(#2243));
#560=EDGE_LOOP('',(#2244,#2245,#2246,#2247));
#561=EDGE_LOOP('',(#2248,#2249,#2250,#2251,#2252,#2253));
#562=EDGE_LOOP('',(#2254,#2255,#2256,#2257));
#563=EDGE_LOOP('',(#2258));
#564=EDGE_LOOP('',(#2259));
#565=EDGE_LOOP('',(#2260));
#566=EDGE_LOOP('',(#2261));
#567=EDGE_LOOP('',(#2262));
#568=EDGE_LOOP('',(#2263));
#569=EDGE_LOOP('',(#2264,#2265,#2266,#2267));
#570=EDGE_LOOP('',(#2268,#2269));
#571=EDGE_LOOP('',(#2270,#2271));
#572=EDGE_LOOP('',(#2272,#2273));
#573=EDGE_LOOP('',(#2274,#2275));
#574=EDGE_LOOP('',(#2276,#2277,#2278,#2279));
#575=EDGE_LOOP('',(#2280,#2281,#2282,#2283));
#576=EDGE_LOOP('',(#2284,#2285,#2286,#2287));
#577=EDGE_LOOP('',(#2288));
#578=EDGE_LOOP('',(#2289));
#579=EDGE_LOOP('',(#2290,#2291,#2292,#2293));
#580=EDGE_LOOP('',(#2294,#2295,#2296,#2297));
#581=EDGE_LOOP('',(#2298,#2299,#2300,#2301));
#582=EDGE_LOOP('',(#2302));
#583=EDGE_LOOP('',(#2303));
#584=EDGE_LOOP('',(#2304,#2305,#2306,#2307,#2308,#2309));
#585=EDGE_LOOP('',(#2310,#2311,#2312,#2313));
#586=EDGE_LOOP('',(#2314,#2315,#2316,#2317));
#587=EDGE_LOOP('',(#2318,#2319,#2320,#2321));
#588=EDGE_LOOP('',(#2322,#2323,#2324,#2325));
#589=EDGE_LOOP('',(#2326,#2327,#2328,#2329,#2330,#2331,#2332,#2333,#2334,
#2335,#2336,#2337,#2338,#2339,#2340,#2341));
#590=EDGE_LOOP('',(#2342));
#591=EDGE_LOOP('',(#2343,#2344,#2345,#2346));
#592=EDGE_LOOP('',(#2347));
#593=EDGE_LOOP('',(#2348));
#594=EDGE_LOOP('',(#2349,#2350,#2351,#2352));
#764=LINE('',#4294,#1018);
#765=LINE('',#4388,#1019);
#766=LINE('',#4394,#1020);
#767=LINE('',#4400,#1021);
#768=LINE('',#4406,#1022);
#769=LINE('',#4500,#1023);
#770=LINE('',#4506,#1024);
#771=LINE('',#4512,#1025);
#772=LINE('',#4525,#1026);
#773=LINE('',#4526,#1027);
#774=LINE('',#4538,#1028);
#775=LINE('',#4539,#1029);
#776=LINE('',#4551,#1030);
#777=LINE('',#4552,#1031);
#778=LINE('',#4554,#1032);
#779=LINE('',#4555,#1033);
#780=LINE('',#4567,#1034);
#781=LINE('',#4568,#1035);
#782=LINE('',#4570,#1036);
#783=LINE('',#4571,#1037);
#784=LINE('',#4573,#1038);
#785=LINE('',#4574,#1039);
#786=LINE('',#4576,#1040);
#787=LINE('',#4577,#1041);
#788=LINE('',#4580,#1042);
#789=LINE('',#4582,#1043);
#790=LINE('',#4584,#1044);
#791=LINE('',#4586,#1045);
#792=LINE('',#4588,#1046);
#793=LINE('',#4590,#1047);
#794=LINE('',#4592,#1048);
#795=LINE('',#4594,#1049);
#796=LINE('',#4596,#1050);
#797=LINE('',#4598,#1051);
#798=LINE('',#4600,#1052);
#799=LINE('',#4602,#1053);
#800=LINE('',#4603,#1054);
#801=LINE('',#4607,#1055);
#802=LINE('',#4610,#1056);
#803=LINE('',#4611,#1057);
#804=LINE('',#4615,#1058);
#805=LINE('',#4620,#1059);
#806=LINE('',#4621,#1060);
#807=LINE('',#4622,#1061);
#808=LINE('',#4626,#1062);
#809=LINE('',#4627,#1063);
#810=LINE('',#4628,#1064);
#811=LINE('',#4630,#1065);
#812=LINE('',#4633,#1066);
#813=LINE('',#4634,#1067);
#814=LINE('',#4638,#1068);
#815=LINE('',#4639,#1069);
#816=LINE('',#4640,#1070);
#817=LINE('',#4642,#1071);
#818=LINE('',#4644,#1072);
#819=LINE('',#4645,#1073);
#820=LINE('',#4648,#1074);
#821=LINE('',#4649,#1075);
#822=LINE('',#4652,#1076);
#823=LINE('',#4653,#1077);
#824=LINE('',#4656,#1078);
#825=LINE('',#4657,#1079);
#826=LINE('',#4660,#1080);
#827=LINE('',#4661,#1081);
#828=LINE('',#4663,#1082);
#1018=VECTOR('',#3533,5.);
#1019=VECTOR('',#3536,5.);
#1020=VECTOR('',#3543,5.);
#1021=VECTOR('',#3550,5.);
#1022=VECTOR('',#3557,5.);
#1023=VECTOR('',#3560,5.);
#1024=VECTOR('',#3567,5.);
#1025=VECTOR('',#3574,5.);
#1026=VECTOR('',#3589,10.);
#1027=VECTOR('',#3590,10.);
#1028=VECTOR('',#3603,10.);
#1029=VECTOR('',#3604,10.);
#1030=VECTOR('',#3617,10.);
#1031=VECTOR('',#3618,10.);
#1032=VECTOR('',#3621,10.);
#1033=VECTOR('',#3622,10.);
#1034=VECTOR('',#3635,10.);
#1035=VECTOR('',#3636,10.);
#1036=VECTOR('',#3639,10.);
#1037=VECTOR('',#3640,10.);
#1038=VECTOR('',#3643,10.);
#1039=VECTOR('',#3644,10.);
#1040=VECTOR('',#3647,10.);
#1041=VECTOR('',#3648,10.);
#1042=VECTOR('',#3651,10.);
#1043=VECTOR('',#3652,10.);
#1044=VECTOR('',#3653,10.);
#1045=VECTOR('',#3654,10.);
#1046=VECTOR('',#3655,10.);
#1047=VECTOR('',#3656,10.);
#1048=VECTOR('',#3657,10.);
#1049=VECTOR('',#3658,10.);
#1050=VECTOR('',#3659,10.);
#1051=VECTOR('',#3660,10.);
#1052=VECTOR('',#3661,10.);
#1053=VECTOR('',#3662,10.);
#1054=VECTOR('',#3663,10.);
#1055=VECTOR('',#3668,10.);
#1056=VECTOR('',#3671,10.);
#1057=VECTOR('',#3672,10.);
#1058=VECTOR('',#3677,6.);
#1059=VECTOR('',#3682,10.);
#1060=VECTOR('',#3683,10.);
#1061=VECTOR('',#3684,10.);
#1062=VECTOR('',#3687,10.);
#1063=VECTOR('',#3688,10.);
#1064=VECTOR('',#3689,10.);
#1065=VECTOR('',#3692,10.);
#1066=VECTOR('',#3695,10.);
#1067=VECTOR('',#3696,10.);
#1068=VECTOR('',#3699,10.);
#1069=VECTOR('',#3700,10.);
#1070=VECTOR('',#3701,10.);
#1071=VECTOR('',#3704,10.);
#1072=VECTOR('',#3707,10.);
#1073=VECTOR('',#3708,10.);
#1074=VECTOR('',#3711,10.);
#1075=VECTOR('',#3712,10.);
#1076=VECTOR('',#3715,10.);
#1077=VECTOR('',#3716,10.);
#1078=VECTOR('',#3719,10.);
#1079=VECTOR('',#3720,10.);
#1080=VECTOR('',#3723,10.);
#1081=VECTOR('',#3724,10.);
#1082=VECTOR('',#3727,10.);
#1167=CIRCLE('',#2972,5.);
#1168=CIRCLE('',#2974,5.);
#1169=CIRCLE('',#2976,5.);
#1170=CIRCLE('',#2977,5.);
#1171=CIRCLE('',#2979,5.);
#1172=CIRCLE('',#2980,5.);
#1173=CIRCLE('',#2982,5.);
#1174=CIRCLE('',#2984,5.);
#1175=CIRCLE('',#2986,5.);
#1176=CIRCLE('',#2987,5.);
#1177=CIRCLE('',#2989,5.);
#1178=CIRCLE('',#2990,5.);
#1179=CIRCLE('',#2992,1.);
#1180=CIRCLE('',#2993,1.00000000000001);
#1181=CIRCLE('',#2994,1.);
#1182=CIRCLE('',#2996,1.);
#1183=CIRCLE('',#2998,0.999999999999996);
#1184=CIRCLE('',#2999,0.999999999999996);
#1185=CIRCLE('',#3000,1.);
#1186=CIRCLE('',#3002,1.);
#1187=CIRCLE('',#3004,0.999999999999996);
#1188=CIRCLE('',#3005,0.999999999999996);
#1189=CIRCLE('',#3006,1.);
#1190=CIRCLE('',#3008,1.);
#1191=CIRCLE('',#3011,0.999999999999996);
#1192=CIRCLE('',#3012,0.999999999999996);
#1193=CIRCLE('',#3013,1.);
#1194=CIRCLE('',#3015,1.);
#1195=CIRCLE('',#3020,6.);
#1196=CIRCLE('',#3025,6.);
#1323=VERTEX_POINT('',#4291);
#1324=VERTEX_POINT('',#4293);
#1325=VERTEX_POINT('',#4295);
#1326=VERTEX_POINT('',#4341);
#1327=VERTEX_POINT('',#4342);
#1328=VERTEX_POINT('',#4387);
#1329=VERTEX_POINT('',#4391);
#1330=VERTEX_POINT('',#4393);
#1331=VERTEX_POINT('',#4397);
#1332=VERTEX_POINT('',#4399);
#1333=VERTEX_POINT('',#4403);
#1334=VERTEX_POINT('',#4405);
#1335=VERTEX_POINT('',#4407);
#1336=VERTEX_POINT('',#4453);
#1337=VERTEX_POINT('',#4454);
#1338=VERTEX_POINT('',#4499);
#1339=VERTEX_POINT('',#4503);
#1340=VERTEX_POINT('',#4505);
#1341=VERTEX_POINT('',#4509);
#1342=VERTEX_POINT('',#4511);
#1343=VERTEX_POINT('',#4515);
#1344=VERTEX_POINT('',#4516);
#1345=VERTEX_POINT('',#4518);
#1346=VERTEX_POINT('',#4522);
#1347=VERTEX_POINT('',#4523);
#1348=VERTEX_POINT('',#4528);
#1349=VERTEX_POINT('',#4529);
#1350=VERTEX_POINT('',#4531);
#1351=VERTEX_POINT('',#4535);
#1352=VERTEX_POINT('',#4536);
#1353=VERTEX_POINT('',#4541);
#1354=VERTEX_POINT('',#4542);
#1355=VERTEX_POINT('',#4544);
#1356=VERTEX_POINT('',#4548);
#1357=VERTEX_POINT('',#4549);
#1358=VERTEX_POINT('',#4557);
#1359=VERTEX_POINT('',#4558);
#1360=VERTEX_POINT('',#4560);
#1361=VERTEX_POINT('',#4564);
#1362=VERTEX_POINT('',#4565);
#1363=VERTEX_POINT('',#4579);
#1364=VERTEX_POINT('',#4581);
#1365=VERTEX_POINT('',#4583);
#1366=VERTEX_POINT('',#4585);
#1367=VERTEX_POINT('',#4587);
#1368=VERTEX_POINT('',#4589);
#1369=VERTEX_POINT('',#4591);
#1370=VERTEX_POINT('',#4593);
#1371=VERTEX_POINT('',#4595);
#1372=VERTEX_POINT('',#4597);
#1373=VERTEX_POINT('',#4599);
#1374=VERTEX_POINT('',#4601);
#1375=VERTEX_POINT('',#4604);
#1376=VERTEX_POINT('',#4609);
#1377=VERTEX_POINT('',#4614);
#1378=VERTEX_POINT('',#4618);
#1379=VERTEX_POINT('',#4619);
#1380=VERTEX_POINT('',#4624);
#1381=VERTEX_POINT('',#4625);
#1382=VERTEX_POINT('',#4632);
#1383=VERTEX_POINT('',#4636);
#1384=VERTEX_POINT('',#4637);
#1385=VERTEX_POINT('',#4647);
#1386=VERTEX_POINT('',#4651);
#1387=VERTEX_POINT('',#4655);
#1388=VERTEX_POINT('',#4659);
#1614=EDGE_CURVE('',#1323,#1323,#1167,.T.);
#1615=EDGE_CURVE('',#1323,#1324,#764,.T.);
#1616=EDGE_CURVE('',#1325,#1324,#59,.T.);
#1617=EDGE_CURVE('',#1324,#1325,#60,.T.);
#1618=EDGE_CURVE('',#1326,#1327,#61,.T.);
#1619=EDGE_CURVE('',#1327,#1326,#62,.T.);
#1620=EDGE_CURVE('',#1327,#1328,#765,.T.);
#1621=EDGE_CURVE('',#1328,#1328,#1168,.T.);
#1622=EDGE_CURVE('',#1329,#1329,#1169,.T.);
#1623=EDGE_CURVE('',#1329,#1330,#766,.T.);
#1624=EDGE_CURVE('',#1330,#1330,#1170,.T.);
#1625=EDGE_CURVE('',#1331,#1331,#1171,.T.);
#1626=EDGE_CURVE('',#1331,#1332,#767,.T.);
#1627=EDGE_CURVE('',#1332,#1332,#1172,.T.);
#1628=EDGE_CURVE('',#1333,#1333,#1173,.T.);
#1629=EDGE_CURVE('',#1333,#1334,#768,.T.);
#1630=EDGE_CURVE('',#1335,#1334,#63,.T.);
#1631=EDGE_CURVE('',#1334,#1335,#64,.T.);
#1632=EDGE_CURVE('',#1336,#1337,#65,.T.);
#1633=EDGE_CURVE('',#1337,#1336,#66,.T.);
#1634=EDGE_CURVE('',#1337,#1338,#769,.T.);
#1635=EDGE_CURVE('',#1338,#1338,#1174,.T.);
#1636=EDGE_CURVE('',#1339,#1339,#1175,.T.);
#1637=EDGE_CURVE('',#1339,#1340,#770,.T.);
#1638=EDGE_CURVE('',#1340,#1340,#1176,.T.);
#1639=EDGE_CURVE('',#1341,#1341,#1177,.T.);
#1640=EDGE_CURVE('',#1341,#1342,#771,.T.);
#1641=EDGE_CURVE('',#1342,#1342,#1178,.T.);
#1642=EDGE_CURVE('',#1343,#1344,#1179,.F.);
#1643=EDGE_CURVE('',#1345,#1343,#1180,.F.);
#1644=EDGE_CURVE('',#1344,#1345,#1181,.F.);
#1645=EDGE_CURVE('',#1346,#1347,#1182,.T.);
#1646=EDGE_CURVE('',#1347,#1345,#772,.T.);
#1647=EDGE_CURVE('',#1343,#1346,#773,.T.);
#1648=EDGE_CURVE('',#1348,#1349,#1183,.F.);
#1649=EDGE_CURVE('',#1350,#1348,#1184,.F.);
#1650=EDGE_CURVE('',#1349,#1350,#1185,.F.);
#1651=EDGE_CURVE('',#1351,#1352,#1186,.T.);
#1652=EDGE_CURVE('',#1352,#1350,#774,.T.);
#1653=EDGE_CURVE('',#1348,#1351,#775,.T.);
#1654=EDGE_CURVE('',#1353,#1354,#1187,.F.);
#1655=EDGE_CURVE('',#1355,#1353,#1188,.F.);
#1656=EDGE_CURVE('',#1354,#1355,#1189,.F.);
#1657=EDGE_CURVE('',#1356,#1357,#1190,.T.);
#1658=EDGE_CURVE('',#1357,#1355,#776,.T.);
#1659=EDGE_CURVE('',#1353,#1356,#777,.T.);
#1660=EDGE_CURVE('',#1344,#1354,#778,.T.);
#1661=EDGE_CURVE('',#1355,#1343,#779,.T.);
#1662=EDGE_CURVE('',#1358,#1359,#1191,.F.);
#1663=EDGE_CURVE('',#1360,#1358,#1192,.F.);
#1664=EDGE_CURVE('',#1359,#1360,#1193,.F.);
#1665=EDGE_CURVE('',#1361,#1362,#1194,.T.);
#1666=EDGE_CURVE('',#1362,#1360,#780,.T.);
#1667=EDGE_CURVE('',#1358,#1361,#781,.T.);
#1668=EDGE_CURVE('',#1354,#1359,#782,.T.);
#1669=EDGE_CURVE('',#1360,#1353,#783,.T.);
#1670=EDGE_CURVE('',#1359,#1349,#784,.T.);
#1671=EDGE_CURVE('',#1350,#1358,#785,.T.);
#1672=EDGE_CURVE('',#1349,#1344,#786,.T.);
#1673=EDGE_CURVE('',#1345,#1348,#787,.T.);
#1674=EDGE_CURVE('',#1357,#1363,#788,.T.);
#1675=EDGE_CURVE('',#1363,#1364,#789,.T.);
#1676=EDGE_CURVE('',#1364,#1365,#790,.T.);
#1677=EDGE_CURVE('',#1365,#1366,#791,.T.);
#1678=EDGE_CURVE('',#1366,#1367,#792,.T.);
#1679=EDGE_CURVE('',#1367,#1368,#793,.T.);
#1680=EDGE_CURVE('',#1369,#1368,#794,.T.);
#1681=EDGE_CURVE('',#1369,#1370,#795,.T.);
#1682=EDGE_CURVE('',#1370,#1371,#796,.T.);
#1683=EDGE_CURVE('',#1371,#1372,#797,.T.);
#1684=EDGE_CURVE('',#1372,#1373,#798,.T.);
#1685=EDGE_CURVE('',#1373,#1374,#799,.T.);
#1686=EDGE_CURVE('',#1374,#1346,#800,.T.);
#1687=EDGE_CURVE('',#1375,#1375,#1195,.T.);
#1688=EDGE_CURVE('',#1362,#1356,#801,.T.);
#1689=EDGE_CURVE('',#1376,#1361,#802,.T.);
#1690=EDGE_CURVE('',#1376,#1363,#803,.T.);
#1691=EDGE_CURVE('',#1375,#1377,#804,.T.);
#1692=EDGE_CURVE('',#1377,#1377,#1196,.T.);
#1693=EDGE_CURVE('',#1378,#1379,#805,.T.);
#1694=EDGE_CURVE('',#1378,#1372,#806,.T.);
#1695=EDGE_CURVE('',#1379,#1371,#807,.T.);
#1696=EDGE_CURVE('',#1380,#1381,#808,.T.);
#1697=EDGE_CURVE('',#1374,#1380,#809,.T.);
#1698=EDGE_CURVE('',#1373,#1381,#810,.T.);
#1699=EDGE_CURVE('',#1381,#1378,#811,.T.);
#1700=EDGE_CURVE('',#1382,#1376,#812,.T.);
#1701=EDGE_CURVE('',#1382,#1364,#813,.T.);
#1702=EDGE_CURVE('',#1383,#1384,#814,.T.);
#1703=EDGE_CURVE('',#1366,#1383,#815,.T.);
#1704=EDGE_CURVE('',#1365,#1384,#816,.T.);
#1705=EDGE_CURVE('',#1384,#1382,#817,.T.);
#1706=EDGE_CURVE('',#1352,#1380,#818,.T.);
#1707=EDGE_CURVE('',#1347,#1351,#819,.T.);
#1708=EDGE_CURVE('',#1385,#1383,#820,.T.);
#1709=EDGE_CURVE('',#1367,#1385,#821,.T.);
#1710=EDGE_CURVE('',#1386,#1370,#822,.T.);
#1711=EDGE_CURVE('',#1379,#1386,#823,.T.);
#1712=EDGE_CURVE('',#1386,#1387,#824,.T.);
#1713=EDGE_CURVE('',#1387,#1369,#825,.T.);
#1714=EDGE_CURVE('',#1388,#1385,#826,.T.);
#1715=EDGE_CURVE('',#1368,#1388,#827,.T.);
#1716=EDGE_CURVE('',#1388,#1387,#828,.T.);
#2147=ORIENTED_EDGE('',*,*,#1614,.F.);
#2148=ORIENTED_EDGE('',*,*,#1615,.T.);
#2149=ORIENTED_EDGE('',*,*,#1616,.F.);
#2150=ORIENTED_EDGE('',*,*,#1617,.F.);
#2151=ORIENTED_EDGE('',*,*,#1615,.F.);
#2152=ORIENTED_EDGE('',*,*,#1618,.F.);
#2153=ORIENTED_EDGE('',*,*,#1619,.F.);
#2154=ORIENTED_EDGE('',*,*,#1620,.T.);
#2155=ORIENTED_EDGE('',*,*,#1621,.F.);
#2156=ORIENTED_EDGE('',*,*,#1620,.F.);
#2157=ORIENTED_EDGE('',*,*,#1622,.F.);
#2158=ORIENTED_EDGE('',*,*,#1623,.T.);
#2159=ORIENTED_EDGE('',*,*,#1624,.F.);
#2160=ORIENTED_EDGE('',*,*,#1623,.F.);
#2161=ORIENTED_EDGE('',*,*,#1625,.F.);
#2162=ORIENTED_EDGE('',*,*,#1626,.T.);
#2163=ORIENTED_EDGE('',*,*,#1627,.F.);
#2164=ORIENTED_EDGE('',*,*,#1626,.F.);
#2165=ORIENTED_EDGE('',*,*,#1628,.F.);
#2166=ORIENTED_EDGE('',*,*,#1629,.T.);
#2167=ORIENTED_EDGE('',*,*,#1630,.F.);
#2168=ORIENTED_EDGE('',*,*,#1631,.F.);
#2169=ORIENTED_EDGE('',*,*,#1629,.F.);
#2170=ORIENTED_EDGE('',*,*,#1632,.F.);
#2171=ORIENTED_EDGE('',*,*,#1633,.F.);
#2172=ORIENTED_EDGE('',*,*,#1634,.T.);
#2173=ORIENTED_EDGE('',*,*,#1635,.F.);
#2174=ORIENTED_EDGE('',*,*,#1634,.F.);
#2175=ORIENTED_EDGE('',*,*,#1636,.F.);
#2176=ORIENTED_EDGE('',*,*,#1637,.T.);
#2177=ORIENTED_EDGE('',*,*,#1638,.F.);
#2178=ORIENTED_EDGE('',*,*,#1637,.F.);
#2179=ORIENTED_EDGE('',*,*,#1639,.F.);
#2180=ORIENTED_EDGE('',*,*,#1640,.T.);
#2181=ORIENTED_EDGE('',*,*,#1641,.F.);
#2182=ORIENTED_EDGE('',*,*,#1640,.F.);
#2183=ORIENTED_EDGE('',*,*,#1642,.F.);
#2184=ORIENTED_EDGE('',*,*,#1643,.F.);
#2185=ORIENTED_EDGE('',*,*,#1644,.F.);
#2186=ORIENTED_EDGE('',*,*,#1645,.T.);
#2187=ORIENTED_EDGE('',*,*,#1646,.T.);
#2188=ORIENTED_EDGE('',*,*,#1643,.T.);
#2189=ORIENTED_EDGE('',*,*,#1647,.T.);
#2190=ORIENTED_EDGE('',*,*,#1648,.F.);
#2191=ORIENTED_EDGE('',*,*,#1649,.F.);
#2192=ORIENTED_EDGE('',*,*,#1650,.F.);
#2193=ORIENTED_EDGE('',*,*,#1651,.T.);
#2194=ORIENTED_EDGE('',*,*,#1652,.T.);
#2195=ORIENTED_EDGE('',*,*,#1649,.T.);
#2196=ORIENTED_EDGE('',*,*,#1653,.T.);
#2197=ORIENTED_EDGE('',*,*,#1654,.F.);
#2198=ORIENTED_EDGE('',*,*,#1655,.F.);
#2199=ORIENTED_EDGE('',*,*,#1656,.F.);
#2200=ORIENTED_EDGE('',*,*,#1657,.T.);
#2201=ORIENTED_EDGE('',*,*,#1658,.T.);
#2202=ORIENTED_EDGE('',*,*,#1655,.T.);
#2203=ORIENTED_EDGE('',*,*,#1659,.T.);
#2204=ORIENTED_EDGE('',*,*,#1642,.T.);
#2205=ORIENTED_EDGE('',*,*,#1660,.T.);
#2206=ORIENTED_EDGE('',*,*,#1656,.T.);
#2207=ORIENTED_EDGE('',*,*,#1661,.T.);
#2208=ORIENTED_EDGE('',*,*,#1662,.F.);
#2209=ORIENTED_EDGE('',*,*,#1663,.F.);
#2210=ORIENTED_EDGE('',*,*,#1664,.F.);
#2211=ORIENTED_EDGE('',*,*,#1665,.T.);
#2212=ORIENTED_EDGE('',*,*,#1666,.T.);
#2213=ORIENTED_EDGE('',*,*,#1663,.T.);
#2214=ORIENTED_EDGE('',*,*,#1667,.T.);
#2215=ORIENTED_EDGE('',*,*,#1654,.T.);
#2216=ORIENTED_EDGE('',*,*,#1668,.T.);
#2217=ORIENTED_EDGE('',*,*,#1664,.T.);
#2218=ORIENTED_EDGE('',*,*,#1669,.T.);
#2219=ORIENTED_EDGE('',*,*,#1662,.T.);
#2220=ORIENTED_EDGE('',*,*,#1670,.T.);
#2221=ORIENTED_EDGE('',*,*,#1650,.T.);
#2222=ORIENTED_EDGE('',*,*,#1671,.T.);
#2223=ORIENTED_EDGE('',*,*,#1648,.T.);
#2224=ORIENTED_EDGE('',*,*,#1672,.T.);
#2225=ORIENTED_EDGE('',*,*,#1644,.T.);
#2226=ORIENTED_EDGE('',*,*,#1673,.T.);
#2227=ORIENTED_EDGE('',*,*,#1647,.F.);
#2228=ORIENTED_EDGE('',*,*,#1661,.F.);
#2229=ORIENTED_EDGE('',*,*,#1658,.F.);
#2230=ORIENTED_EDGE('',*,*,#1674,.T.);
#2231=ORIENTED_EDGE('',*,*,#1675,.T.);
#2232=ORIENTED_EDGE('',*,*,#1676,.T.);
#2233=ORIENTED_EDGE('',*,*,#1677,.T.);
#2234=ORIENTED_EDGE('',*,*,#1678,.T.);
#2235=ORIENTED_EDGE('',*,*,#1679,.T.);
#2236=ORIENTED_EDGE('',*,*,#1680,.F.);
#2237=ORIENTED_EDGE('',*,*,#1681,.T.);
#2238=ORIENTED_EDGE('',*,*,#1682,.T.);
#2239=ORIENTED_EDGE('',*,*,#1683,.T.);
#2240=ORIENTED_EDGE('',*,*,#1684,.T.);
#2241=ORIENTED_EDGE('',*,*,#1685,.T.);
#2242=ORIENTED_EDGE('',*,*,#1686,.T.);
#2243=ORIENTED_EDGE('',*,*,#1687,.T.);
#2244=ORIENTED_EDGE('',*,*,#1659,.F.);
#2245=ORIENTED_EDGE('',*,*,#1669,.F.);
#2246=ORIENTED_EDGE('',*,*,#1666,.F.);
#2247=ORIENTED_EDGE('',*,*,#1688,.T.);
#2248=ORIENTED_EDGE('',*,*,#1657,.F.);
#2249=ORIENTED_EDGE('',*,*,#1688,.F.);
#2250=ORIENTED_EDGE('',*,*,#1665,.F.);
#2251=ORIENTED_EDGE('',*,*,#1689,.F.);
#2252=ORIENTED_EDGE('',*,*,#1690,.T.);
#2253=ORIENTED_EDGE('',*,*,#1674,.F.);
#2254=ORIENTED_EDGE('',*,*,#1660,.F.);
#2255=ORIENTED_EDGE('',*,*,#1672,.F.);
#2256=ORIENTED_EDGE('',*,*,#1670,.F.);
#2257=ORIENTED_EDGE('',*,*,#1668,.F.);
#2258=ORIENTED_EDGE('',*,*,#1639,.T.);
#2259=ORIENTED_EDGE('',*,*,#1636,.T.);
#2260=ORIENTED_EDGE('',*,*,#1628,.T.);
#2261=ORIENTED_EDGE('',*,*,#1625,.T.);
#2262=ORIENTED_EDGE('',*,*,#1622,.T.);
#2263=ORIENTED_EDGE('',*,*,#1614,.T.);
#2264=ORIENTED_EDGE('',*,*,#1687,.F.);
#2265=ORIENTED_EDGE('',*,*,#1691,.T.);
#2266=ORIENTED_EDGE('',*,*,#1692,.F.);
#2267=ORIENTED_EDGE('',*,*,#1691,.F.);
#2268=ORIENTED_EDGE('',*,*,#1618,.T.);
#2269=ORIENTED_EDGE('',*,*,#1619,.T.);
#2270=ORIENTED_EDGE('',*,*,#1616,.T.);
#2271=ORIENTED_EDGE('',*,*,#1617,.T.);
#2272=ORIENTED_EDGE('',*,*,#1632,.T.);
#2273=ORIENTED_EDGE('',*,*,#1633,.T.);
#2274=ORIENTED_EDGE('',*,*,#1630,.T.);
#2275=ORIENTED_EDGE('',*,*,#1631,.T.);
#2276=ORIENTED_EDGE('',*,*,#1693,.F.);
#2277=ORIENTED_EDGE('',*,*,#1694,.T.);
#2278=ORIENTED_EDGE('',*,*,#1683,.F.);
#2279=ORIENTED_EDGE('',*,*,#1695,.F.);
#2280=ORIENTED_EDGE('',*,*,#1696,.F.);
#2281=ORIENTED_EDGE('',*,*,#1697,.F.);
#2282=ORIENTED_EDGE('',*,*,#1685,.F.);
#2283=ORIENTED_EDGE('',*,*,#1698,.T.);
#2284=ORIENTED_EDGE('',*,*,#1699,.F.);
#2285=ORIENTED_EDGE('',*,*,#1698,.F.);
#2286=ORIENTED_EDGE('',*,*,#1684,.F.);
#2287=ORIENTED_EDGE('',*,*,#1694,.F.);
#2288=ORIENTED_EDGE('',*,*,#1624,.T.);
#2289=ORIENTED_EDGE('',*,*,#1638,.T.);
#2290=ORIENTED_EDGE('',*,*,#1700,.F.);
#2291=ORIENTED_EDGE('',*,*,#1701,.T.);
#2292=ORIENTED_EDGE('',*,*,#1675,.F.);
#2293=ORIENTED_EDGE('',*,*,#1690,.F.);
#2294=ORIENTED_EDGE('',*,*,#1702,.F.);
#2295=ORIENTED_EDGE('',*,*,#1703,.F.);
#2296=ORIENTED_EDGE('',*,*,#1677,.F.);
#2297=ORIENTED_EDGE('',*,*,#1704,.T.);
#2298=ORIENTED_EDGE('',*,*,#1705,.F.);
#2299=ORIENTED_EDGE('',*,*,#1704,.F.);
#2300=ORIENTED_EDGE('',*,*,#1676,.F.);
#2301=ORIENTED_EDGE('',*,*,#1701,.F.);
#2302=ORIENTED_EDGE('',*,*,#1627,.T.);
#2303=ORIENTED_EDGE('',*,*,#1641,.T.);
#2304=ORIENTED_EDGE('',*,*,#1645,.F.);
#2305=ORIENTED_EDGE('',*,*,#1686,.F.);
#2306=ORIENTED_EDGE('',*,*,#1697,.T.);
#2307=ORIENTED_EDGE('',*,*,#1706,.F.);
#2308=ORIENTED_EDGE('',*,*,#1651,.F.);
#2309=ORIENTED_EDGE('',*,*,#1707,.F.);
#2310=ORIENTED_EDGE('',*,*,#1703,.T.);
#2311=ORIENTED_EDGE('',*,*,#1708,.F.);
#2312=ORIENTED_EDGE('',*,*,#1709,.F.);
#2313=ORIENTED_EDGE('',*,*,#1678,.F.);
#2314=ORIENTED_EDGE('',*,*,#1695,.T.);
#2315=ORIENTED_EDGE('',*,*,#1682,.F.);
#2316=ORIENTED_EDGE('',*,*,#1710,.F.);
#2317=ORIENTED_EDGE('',*,*,#1711,.F.);
#2318=ORIENTED_EDGE('',*,*,#1712,.F.);
#2319=ORIENTED_EDGE('',*,*,#1710,.T.);
#2320=ORIENTED_EDGE('',*,*,#1681,.F.);
#2321=ORIENTED_EDGE('',*,*,#1713,.F.);
#2322=ORIENTED_EDGE('',*,*,#1714,.F.);
#2323=ORIENTED_EDGE('',*,*,#1715,.F.);
#2324=ORIENTED_EDGE('',*,*,#1679,.F.);
#2325=ORIENTED_EDGE('',*,*,#1709,.T.);
#2326=ORIENTED_EDGE('',*,*,#1652,.F.);
#2327=ORIENTED_EDGE('',*,*,#1706,.T.);
#2328=ORIENTED_EDGE('',*,*,#1696,.T.);
#2329=ORIENTED_EDGE('',*,*,#1699,.T.);
#2330=ORIENTED_EDGE('',*,*,#1693,.T.);
#2331=ORIENTED_EDGE('',*,*,#1711,.T.);
#2332=ORIENTED_EDGE('',*,*,#1712,.T.);
#2333=ORIENTED_EDGE('',*,*,#1716,.F.);
#2334=ORIENTED_EDGE('',*,*,#1714,.T.);
#2335=ORIENTED_EDGE('',*,*,#1708,.T.);
#2336=ORIENTED_EDGE('',*,*,#1702,.T.);
#2337=ORIENTED_EDGE('',*,*,#1705,.T.);
#2338=ORIENTED_EDGE('',*,*,#1700,.T.);
#2339=ORIENTED_EDGE('',*,*,#1689,.T.);
#2340=ORIENTED_EDGE('',*,*,#1667,.F.);
#2341=ORIENTED_EDGE('',*,*,#1671,.F.);
#2342=ORIENTED_EDGE('',*,*,#1692,.T.);
#2343=ORIENTED_EDGE('',*,*,#1713,.T.);
#2344=ORIENTED_EDGE('',*,*,#1680,.T.);
#2345=ORIENTED_EDGE('',*,*,#1715,.T.);
#2346=ORIENTED_EDGE('',*,*,#1716,.T.);
#2347=ORIENTED_EDGE('',*,*,#1621,.T.);
#2348=ORIENTED_EDGE('',*,*,#1635,.T.);
#2349=ORIENTED_EDGE('',*,*,#1646,.F.);
#2350=ORIENTED_EDGE('',*,*,#1707,.T.);
#2351=ORIENTED_EDGE('',*,*,#1653,.F.);
#2352=ORIENTED_EDGE('',*,*,#1673,.F.);
#2505=CYLINDRICAL_SURFACE('',#2971,5.);
#2506=CYLINDRICAL_SURFACE('',#2973,5.);
#2507=CYLINDRICAL_SURFACE('',#2975,5.);
#2508=CYLINDRICAL_SURFACE('',#2978,5.);
#2509=CYLINDRICAL_SURFACE('',#2981,5.);
#2510=CYLINDRICAL_SURFACE('',#2983,5.);
#2511=CYLINDRICAL_SURFACE('',#2985,5.);
#2512=CYLINDRICAL_SURFACE('',#2988,5.);
#2513=CYLINDRICAL_SURFACE('',#2995,1.);
#2514=CYLINDRICAL_SURFACE('',#3001,1.);
#2515=CYLINDRICAL_SURFACE('',#3007,1.);
#2516=CYLINDRICAL_SURFACE('',#3009,1.);
#2517=CYLINDRICAL_SURFACE('',#3014,1.);
#2518=CYLINDRICAL_SURFACE('',#3016,1.);
#2519=CYLINDRICAL_SURFACE('',#3017,1.);
#2520=CYLINDRICAL_SURFACE('',#3018,1.);
#2521=CYLINDRICAL_SURFACE('',#3024,6.);
#2620=ADVANCED_FACE('',(#362),#2505,.F.);
#2621=ADVANCED_FACE('',(#363),#2506,.F.);
#2622=ADVANCED_FACE('',(#364),#2507,.F.);
#2623=ADVANCED_FACE('',(#365),#2508,.F.);
#2624=ADVANCED_FACE('',(#366),#2509,.F.);
#2625=ADVANCED_FACE('',(#367),#2510,.F.);
#2626=ADVANCED_FACE('',(#368),#2511,.F.);
#2627=ADVANCED_FACE('',(#369),#2512,.F.);
#2628=ADVANCED_FACE('',(#370),#55,.T.);
#2629=ADVANCED_FACE('',(#371),#2513,.T.);
#2630=ADVANCED_FACE('',(#372),#56,.T.);
#2631=ADVANCED_FACE('',(#373),#2514,.T.);
#2632=ADVANCED_FACE('',(#374),#57,.T.);
#2633=ADVANCED_FACE('',(#375),#2515,.T.);
#2634=ADVANCED_FACE('',(#376),#2516,.T.);
#2635=ADVANCED_FACE('',(#377),#58,.T.);
#2636=ADVANCED_FACE('',(#378),#2517,.T.);
#2637=ADVANCED_FACE('',(#379),#2518,.T.);
#2638=ADVANCED_FACE('',(#380),#2519,.T.);
#2639=ADVANCED_FACE('',(#381),#2520,.T.);
#2640=ADVANCED_FACE('',(#382,#142),#226,.T.);
#2641=ADVANCED_FACE('',(#383),#227,.T.);
#2642=ADVANCED_FACE('',(#384),#228,.F.);
#2643=ADVANCED_FACE('',(#385,#143,#144,#145,#146,#147,#148),#229,.T.);
#2644=ADVANCED_FACE('',(#386,#149,#150,#151,#152),#2521,.F.);
#2645=ADVANCED_FACE('',(#387),#230,.F.);
#2646=ADVANCED_FACE('',(#388),#231,.F.);
#2647=ADVANCED_FACE('',(#389,#153,#154),#232,.F.);
#2648=ADVANCED_FACE('',(#390),#233,.F.);
#2649=ADVANCED_FACE('',(#391),#234,.F.);
#2650=ADVANCED_FACE('',(#392,#155,#156),#235,.F.);
#2651=ADVANCED_FACE('',(#393),#236,.F.);
#2652=ADVANCED_FACE('',(#394),#237,.F.);
#2653=ADVANCED_FACE('',(#395),#238,.F.);
#2654=ADVANCED_FACE('',(#396),#239,.F.);
#2655=ADVANCED_FACE('',(#397),#240,.F.);
#2656=ADVANCED_FACE('',(#398,#157),#241,.T.);
#2657=ADVANCED_FACE('',(#399,#158,#159),#242,.F.);
#2658=ADVANCED_FACE('',(#400),#243,.T.);
#2694=CLOSED_SHELL('',(#2620,#2621,#2622,#2623,#2624,#2625,#2626,#2627,
#2628,#2629,#2630,#2631,#2632,#2633,#2634,#2635,#2636,#2637,#2638,#2639,
#2640,#2641,#2642,#2643,#2644,#2645,#2646,#2647,#2648,#2649,#2650,#2651,
#2652,#2653,#2654,#2655,#2656,#2657,#2658));
#2970=AXIS2_PLACEMENT_3D('',#4289,#3527,#3528);
#2971=AXIS2_PLACEMENT_3D('',#4290,#3529,#3530);
#2972=AXIS2_PLACEMENT_3D('',#4292,#3531,#3532);
#2973=AXIS2_PLACEMENT_3D('',#4340,#3534,#3535);
#2974=AXIS2_PLACEMENT_3D('',#4389,#3537,#3538);
#2975=AXIS2_PLACEMENT_3D('',#4390,#3539,#3540);
#2976=AXIS2_PLACEMENT_3D('',#4392,#3541,#3542);
#2977=AXIS2_PLACEMENT_3D('',#4395,#3544,#3545);
#2978=AXIS2_PLACEMENT_3D('',#4396,#3546,#3547);
#2979=AXIS2_PLACEMENT_3D('',#4398,#3548,#3549);
#2980=AXIS2_PLACEMENT_3D('',#4401,#3551,#3552);
#2981=AXIS2_PLACEMENT_3D('',#4402,#3553,#3554);
#2982=AXIS2_PLACEMENT_3D('',#4404,#3555,#3556);
#2983=AXIS2_PLACEMENT_3D('',#4452,#3558,#3559);
#2984=AXIS2_PLACEMENT_3D('',#4501,#3561,#3562);
#2985=AXIS2_PLACEMENT_3D('',#4502,#3563,#3564);
#2986=AXIS2_PLACEMENT_3D('',#4504,#3565,#3566);
#2987=AXIS2_PLACEMENT_3D('',#4507,#3568,#3569);
#2988=AXIS2_PLACEMENT_3D('',#4508,#3570,#3571);
#2989=AXIS2_PLACEMENT_3D('',#4510,#3572,#3573);
#2990=AXIS2_PLACEMENT_3D('',#4513,#3575,#3576);
#2991=AXIS2_PLACEMENT_3D('',#4514,#3577,#3578);
#2992=AXIS2_PLACEMENT_3D('',#4517,#3579,#3580);
#2993=AXIS2_PLACEMENT_3D('',#4519,#3581,#3582);
#2994=AXIS2_PLACEMENT_3D('',#4520,#3583,#3584);
#2995=AXIS2_PLACEMENT_3D('',#4521,#3585,#3586);
#2996=AXIS2_PLACEMENT_3D('',#4524,#3587,#3588);
#2997=AXIS2_PLACEMENT_3D('',#4527,#3591,#3592);
#2998=AXIS2_PLACEMENT_3D('',#4530,#3593,#3594);
#2999=AXIS2_PLACEMENT_3D('',#4532,#3595,#3596);
#3000=AXIS2_PLACEMENT_3D('',#4533,#3597,#3598);
#3001=AXIS2_PLACEMENT_3D('',#4534,#3599,#3600);
#3002=AXIS2_PLACEMENT_3D('',#4537,#3601,#3602);
#3003=AXIS2_PLACEMENT_3D('',#4540,#3605,#3606);
#3004=AXIS2_PLACEMENT_3D('',#4543,#3607,#3608);
#3005=AXIS2_PLACEMENT_3D('',#4545,#3609,#3610);
#3006=AXIS2_PLACEMENT_3D('',#4546,#3611,#3612);
#3007=AXIS2_PLACEMENT_3D('',#4547,#3613,#3614);
#3008=AXIS2_PLACEMENT_3D('',#4550,#3615,#3616);
#3009=AXIS2_PLACEMENT_3D('',#4553,#3619,#3620);
#3010=AXIS2_PLACEMENT_3D('',#4556,#3623,#3624);
#3011=AXIS2_PLACEMENT_3D('',#4559,#3625,#3626);
#3012=AXIS2_PLACEMENT_3D('',#4561,#3627,#3628);
#3013=AXIS2_PLACEMENT_3D('',#4562,#3629,#3630);
#3014=AXIS2_PLACEMENT_3D('',#4563,#3631,#3632);
#3015=AXIS2_PLACEMENT_3D('',#4566,#3633,#3634);
#3016=AXIS2_PLACEMENT_3D('',#4569,#3637,#3638);
#3017=AXIS2_PLACEMENT_3D('',#4572,#3641,#3642);
#3018=AXIS2_PLACEMENT_3D('',#4575,#3645,#3646);
#3019=AXIS2_PLACEMENT_3D('',#4578,#3649,#3650);
#3020=AXIS2_PLACEMENT_3D('',#4605,#3664,#3665);
#3021=AXIS2_PLACEMENT_3D('',#4606,#3666,#3667);
#3022=AXIS2_PLACEMENT_3D('',#4608,#3669,#3670);
#3023=AXIS2_PLACEMENT_3D('',#4612,#3673,#3674);
#3024=AXIS2_PLACEMENT_3D('',#4613,#3675,#3676);
#3025=AXIS2_PLACEMENT_3D('',#4616,#3678,#3679);
#3026=AXIS2_PLACEMENT_3D('',#4617,#3680,#3681);
#3027=AXIS2_PLACEMENT_3D('',#4623,#3685,#3686);
#3028=AXIS2_PLACEMENT_3D('',#4629,#3690,#3691);
#3029=AXIS2_PLACEMENT_3D('',#4631,#3693,#3694);
#3030=AXIS2_PLACEMENT_3D('',#4635,#3697,#3698);
#3031=AXIS2_PLACEMENT_3D('',#4641,#3702,#3703);
#3032=AXIS2_PLACEMENT_3D('',#4643,#3705,#3706);
#3033=AXIS2_PLACEMENT_3D('',#4646,#3709,#3710);
#3034=AXIS2_PLACEMENT_3D('',#4650,#3713,#3714);
#3035=AXIS2_PLACEMENT_3D('',#4654,#3717,#3718);
#3036=AXIS2_PLACEMENT_3D('',#4658,#3721,#3722);
#3037=AXIS2_PLACEMENT_3D('',#4662,#3725,#3726);
#3038=AXIS2_PLACEMENT_3D('',#4664,#3728,#3729);
#3039=AXIS2_PLACEMENT_3D('',#4665,#3730,#3731);
#3527=DIRECTION('axis',(0.,0.,1.));
#3528=DIRECTION('refdir',(1.,0.,0.));
#3529=DIRECTION('center_axis',(0.,0.,-1.));
#3530=DIRECTION('ref_axis',(-1.,0.,0.));
#3531=DIRECTION('center_axis',(0.,0.,-1.));
#3532=DIRECTION('ref_axis',(-1.,0.,0.));
#3533=DIRECTION('',(0.,0.,-1.));
#3534=DIRECTION('center_axis',(0.,0.,-1.));
#3535=DIRECTION('ref_axis',(-1.,0.,0.));
#3536=DIRECTION('',(0.,0.,-1.));
#3537=DIRECTION('center_axis',(0.,0.,1.));
#3538=DIRECTION('ref_axis',(-1.,0.,0.));
#3539=DIRECTION('center_axis',(0.,0.,-1.));
#3540=DIRECTION('ref_axis',(-1.,0.,0.));
#3541=DIRECTION('center_axis',(0.,0.,-1.));
#3542=DIRECTION('ref_axis',(-1.,0.,0.));
#3543=DIRECTION('',(0.,0.,-1.));
#3544=DIRECTION('center_axis',(0.,0.,1.));
#3545=DIRECTION('ref_axis',(-1.,0.,0.));
#3546=DIRECTION('center_axis',(0.,0.,-1.));
#3547=DIRECTION('ref_axis',(-1.,0.,0.));
#3548=DIRECTION('center_axis',(0.,0.,-1.));
#3549=DIRECTION('ref_axis',(-1.,0.,0.));
#3550=DIRECTION('',(0.,0.,-1.));
#3551=DIRECTION('center_axis',(0.,0.,1.));
#3552=DIRECTION('ref_axis',(-1.,0.,0.));
#3553=DIRECTION('center_axis',(0.,0.,-1.));
#3554=DIRECTION('ref_axis',(-1.,0.,0.));
#3555=DIRECTION('center_axis',(0.,0.,-1.));
#3556=DIRECTION('ref_axis',(-1.,0.,0.));
#3557=DIRECTION('',(0.,0.,-1.));
#3558=DIRECTION('center_axis',(0.,0.,-1.));
#3559=DIRECTION('ref_axis',(-1.,0.,0.));
#3560=DIRECTION('',(0.,0.,-1.));
#3561=DIRECTION('center_axis',(0.,0.,1.));
#3562=DIRECTION('ref_axis',(-1.,0.,0.));
#3563=DIRECTION('center_axis',(0.,0.,-1.));
#3564=DIRECTION('ref_axis',(-1.,0.,0.));
#3565=DIRECTION('center_axis',(0.,0.,-1.));
#3566=DIRECTION('ref_axis',(-1.,0.,0.));
#3567=DIRECTION('',(0.,0.,-1.));
#3568=DIRECTION('center_axis',(0.,0.,1.));
#3569=DIRECTION('ref_axis',(-1.,0.,0.));
#3570=DIRECTION('center_axis',(0.,0.,-1.));
#3571=DIRECTION('ref_axis',(-1.,0.,0.));
#3572=DIRECTION('center_axis',(0.,0.,-1.));
#3573=DIRECTION('ref_axis',(-1.,0.,0.));
#3574=DIRECTION('',(0.,0.,-1.));
#3575=DIRECTION('center_axis',(0.,0.,1.));
#3576=DIRECTION('ref_axis',(-1.,0.,0.));
#3577=DIRECTION('center_axis',(-0.816496580927728,0.408248290463864,0.408248290463857));
#3578=DIRECTION('ref_axis',(0.57735026918962,0.577350269189634,0.577350269189623));
#3579=DIRECTION('center_axis',(0.,1.,-1.77635683940025E-14));
#3580=DIRECTION('ref_axis',(1.,0.,0.));
#3581=DIRECTION('center_axis',(0.,0.,1.));
#3582=DIRECTION('ref_axis',(0.,1.,0.));
#3583=DIRECTION('center_axis',(1.,-4.44089209850064E-15,0.));
#3584=DIRECTION('ref_axis',(0.,0.,1.));
#3585=DIRECTION('center_axis',(0.,0.,1.));
#3586=DIRECTION('ref_axis',(0.707106781186544,0.707106781186551,0.));
#3587=DIRECTION('center_axis',(0.,0.,1.));
#3588=DIRECTION('ref_axis',(0.707106781186544,0.707106781186551,0.));
#3589=DIRECTION('',(0.,0.,1.));
#3590=DIRECTION('',(0.,0.,-1.));
#3591=DIRECTION('center_axis',(-0.408248290463861,-0.816496580927726,0.408248290463865));
#3592=DIRECTION('ref_axis',(-0.577350269189626,0.577350269189626,0.577350269189626));
#3593=DIRECTION('center_axis',(-1.,0.,0.));
#3594=DIRECTION('ref_axis',(0.,1.,0.));
#3595=DIRECTION('center_axis',(0.,0.,1.));
#3596=DIRECTION('ref_axis',(-1.,0.,0.));
#3597=DIRECTION('center_axis',(0.,1.,0.));
#3598=DIRECTION('ref_axis',(0.,0.,1.));
#3599=DIRECTION('center_axis',(0.,0.,1.));
#3600=DIRECTION('ref_axis',(-0.707106781186548,0.707106781186548,0.));
#3601=DIRECTION('center_axis',(0.,0.,1.));
#3602=DIRECTION('ref_axis',(-0.707106781186548,0.707106781186548,0.));
#3603=DIRECTION('',(0.,0.,1.));
#3604=DIRECTION('',(0.,0.,-1.));
#3605=DIRECTION('center_axis',(-0.816496580927733,-0.408248290463861,0.408248290463851));
#3606=DIRECTION('ref_axis',(0.577350269189619,-0.57735026918964,0.577350269189619));
#3607=DIRECTION('center_axis',(1.,0.,0.));
#3608=DIRECTION('ref_axis',(0.,-1.,0.));
#3609=DIRECTION('center_axis',(0.,0.,1.));
#3610=DIRECTION('ref_axis',(1.,0.,0.));
#3611=DIRECTION('center_axis',(1.77635683940025E-14,-1.,0.));
#3612=DIRECTION('ref_axis',(0.,0.,1.));
#3613=DIRECTION('center_axis',(0.,0.,1.));
#3614=DIRECTION('ref_axis',(0.707106781186541,-0.707106781186554,0.));
#3615=DIRECTION('center_axis',(0.,0.,1.));
#3616=DIRECTION('ref_axis',(0.707106781186541,-0.707106781186554,0.));
#3617=DIRECTION('',(0.,0.,1.));
#3618=DIRECTION('',(0.,0.,-1.));
#3619=DIRECTION('center_axis',(0.,1.,0.));
#3620=DIRECTION('ref_axis',(0.707106781186549,0.,0.707106781186546));
#3621=DIRECTION('',(0.,-1.,0.));
#3622=DIRECTION('',(0.,1.,0.));
#3623=DIRECTION('center_axis',(0.408248290463862,-0.816496580927725,-0.408248290463866));
#3624=DIRECTION('ref_axis',(-0.577350269189626,-0.577350269189626,0.577350269189626));
#3625=DIRECTION('center_axis',(0.,-1.,0.));
#3626=DIRECTION('ref_axis',(-1.,0.,0.));
#3627=DIRECTION('center_axis',(0.,0.,1.));
#3628=DIRECTION('ref_axis',(0.,-1.,0.));
#3629=DIRECTION('center_axis',(-1.,0.,0.));
#3630=DIRECTION('ref_axis',(0.,0.,1.));
#3631=DIRECTION('center_axis',(0.,0.,1.));
#3632=DIRECTION('ref_axis',(-0.707106781186554,-0.707106781186541,0.));
#3633=DIRECTION('center_axis',(0.,0.,1.));
#3634=DIRECTION('ref_axis',(-0.707106781186554,-0.707106781186541,0.));
#3635=DIRECTION('',(0.,0.,1.));
#3636=DIRECTION('',(0.,0.,-1.));
#3637=DIRECTION('center_axis',(1.,0.,0.));
#3638=DIRECTION('ref_axis',(0.,-0.70710678118654,0.707106781186555));
#3639=DIRECTION('',(-1.,0.,0.));
#3640=DIRECTION('',(1.,0.,0.));
#3641=DIRECTION('center_axis',(0.,-1.,0.));
#3642=DIRECTION('ref_axis',(-0.707106781186546,0.,0.707106781186549));
#3643=DIRECTION('',(0.,1.,0.));
#3644=DIRECTION('',(0.,-1.,0.));
#3645=DIRECTION('center_axis',(-1.,0.,0.));
#3646=DIRECTION('ref_axis',(0.,0.707106781186546,0.707106781186549));
#3647=DIRECTION('',(1.,0.,0.));
#3648=DIRECTION('',(-1.,0.,0.));
#3649=DIRECTION('center_axis',(1.,0.,0.));
#3650=DIRECTION('ref_axis',(0.,1.,0.));
#3651=DIRECTION('',(0.,1.,0.));
#3652=DIRECTION('',(0.,0.,1.));
#3653=DIRECTION('',(0.,1.,0.));
#3654=DIRECTION('',(0.,0.,-1.));
#3655=DIRECTION('',(0.,1.,0.));
#3656=DIRECTION('',(0.,0.,-1.));
#3657=DIRECTION('',(0.,-1.,0.));
#3658=DIRECTION('',(0.,0.,1.));
#3659=DIRECTION('',(0.,1.,0.));
#3660=DIRECTION('',(0.,0.,1.));
#3661=DIRECTION('',(0.,1.,0.));
#3662=DIRECTION('',(0.,0.,-1.));
#3663=DIRECTION('',(0.,1.,0.));
#3664=DIRECTION('center_axis',(-1.,0.,0.));
#3665=DIRECTION('ref_axis',(0.,-1.,0.));
#3666=DIRECTION('center_axis',(0.,-1.,0.));
#3667=DIRECTION('ref_axis',(1.,0.,0.));
#3668=DIRECTION('',(1.,0.,0.));
#3669=DIRECTION('center_axis',(0.,0.,1.));
#3670=DIRECTION('ref_axis',(1.,0.,0.));
#3671=DIRECTION('',(0.,-1.,0.));
#3672=DIRECTION('',(1.,0.,0.));
#3673=DIRECTION('center_axis',(0.,0.,1.));
#3674=DIRECTION('ref_axis',(1.,0.,0.));
#3675=DIRECTION('center_axis',(-1.,0.,0.));
#3676=DIRECTION('ref_axis',(0.,-1.,0.));
#3677=DIRECTION('',(-1.,0.,0.));
#3678=DIRECTION('center_axis',(1.,0.,0.));
#3679=DIRECTION('ref_axis',(0.,-1.,0.));
#3680=DIRECTION('center_axis',(0.,-1.,0.));
#3681=DIRECTION('ref_axis',(1.,0.,0.));
#3682=DIRECTION('',(0.,0.,-1.));
#3683=DIRECTION('',(1.,0.,0.));
#3684=DIRECTION('',(1.,0.,0.));
#3685=DIRECTION('center_axis',(0.,1.,0.));
#3686=DIRECTION('ref_axis',(-1.,0.,0.));
#3687=DIRECTION('',(0.,0.,1.));
#3688=DIRECTION('',(-1.,0.,0.));
#3689=DIRECTION('',(-1.,0.,0.));
#3690=DIRECTION('center_axis',(0.,0.,1.));
#3691=DIRECTION('ref_axis',(1.,0.,0.));
#3692=DIRECTION('',(0.,-1.,0.));
#3693=DIRECTION('center_axis',(0.,-1.,0.));
#3694=DIRECTION('ref_axis',(1.,0.,0.));
#3695=DIRECTION('',(0.,0.,-1.));
#3696=DIRECTION('',(1.,0.,0.));
#3697=DIRECTION('center_axis',(0.,1.,0.));
#3698=DIRECTION('ref_axis',(-1.,0.,0.));
#3699=DIRECTION('',(0.,0.,1.));
#3700=DIRECTION('',(-1.,0.,0.));
#3701=DIRECTION('',(-1.,0.,0.));
#3702=DIRECTION('center_axis',(0.,0.,1.));
#3703=DIRECTION('ref_axis',(1.,0.,0.));
#3704=DIRECTION('',(0.,-1.,0.));
#3705=DIRECTION('center_axis',(0.,0.,1.));
#3706=DIRECTION('ref_axis',(1.,0.,0.));
#3707=DIRECTION('',(0.,-1.,0.));
#3708=DIRECTION('',(-1.,0.,0.));
#3709=DIRECTION('center_axis',(0.,0.,1.));
#3710=DIRECTION('ref_axis',(1.,0.,0.));
#3711=DIRECTION('',(0.,-1.,0.));
#3712=DIRECTION('',(-1.,0.,0.));
#3713=DIRECTION('center_axis',(0.,0.,1.));
#3714=DIRECTION('ref_axis',(1.,0.,0.));
#3715=DIRECTION('',(1.,0.,0.));
#3716=DIRECTION('',(0.,-1.,0.));
#3717=DIRECTION('center_axis',(0.,-1.,0.));
#3718=DIRECTION('ref_axis',(1.,0.,0.));
#3719=DIRECTION('',(0.,0.,-1.));
#3720=DIRECTION('',(1.,0.,0.));
#3721=DIRECTION('center_axis',(0.,1.,0.));
#3722=DIRECTION('ref_axis',(-1.,0.,0.));
#3723=DIRECTION('',(0.,0.,1.));
#3724=DIRECTION('',(-1.,0.,0.));
#3725=DIRECTION('center_axis',(-1.,0.,0.));
#3726=DIRECTION('ref_axis',(0.,-1.,0.));
#3727=DIRECTION('',(0.,1.,0.));
#3728=DIRECTION('center_axis',(0.,0.,1.));
#3729=DIRECTION('ref_axis',(-1.,0.,0.));
#3730=DIRECTION('center_axis',(0.,1.,0.));
#3731=DIRECTION('ref_axis',(-1.,0.,0.));
#4289=CARTESIAN_POINT('',(0.,0.,0.));
#4290=CARTESIAN_POINT('Origin',(-34.3120542422792,-30.0000000000105,20.0000000000021));
#4291=CARTESIAN_POINT('',(-29.3120542422792,-30.0000000000105,20.0000000000021));
#4292=CARTESIAN_POINT('Origin',(-34.3120542422792,-30.0000000000105,20.0000000000021));
#4293=CARTESIAN_POINT('',(-29.3120542422792,-30.0000000000105,13.0000000000021));
#4294=CARTESIAN_POINT('',(-29.3120542422792,-30.0000000000105,20.0000000000021));
#4295=CARTESIAN_POINT('',(-34.3120542422792,-35.0000000000105,10.3166247903575));
#4296=CARTESIAN_POINT('Ctrl Pts',(-34.3120542422792,-35.0000000000105,10.3166247903575));
#4297=CARTESIAN_POINT('Ctrl Pts',(-33.9649654150723,-35.0000000000105,10.3166247903575));
#4298=CARTESIAN_POINT('Ctrl Pts',(-33.6249191325797,-34.9638640057048,10.372517968392));
#4299=CARTESIAN_POINT('Ctrl Pts',(-32.9692326416159,-34.8279323440191,10.564392312562));
#4300=CARTESIAN_POINT('Ctrl Pts',(-32.6532784827973,-34.7281094760039,10.6992796672134));
#4301=CARTESIAN_POINT('Ctrl Pts',(-31.7522928141166,-34.3444039514126,11.1575129861594));
#4302=CARTESIAN_POINT('Ctrl Pts',(-31.2127810222979,-33.9717945918947,11.5295040511826));
#4303=CARTESIAN_POINT('Ctrl Pts',(-30.3579885926001,-33.1170021621969,12.1529255036342));
#4304=CARTESIAN_POINT('Ctrl Pts',(-29.9764667659311,-32.5780383625098,12.4565421384626));
#4305=CARTESIAN_POINT('Ctrl Pts',(-29.4527956614068,-31.3532217388044,12.8812351576426));
#4306=CARTESIAN_POINT('Ctrl Pts',(-29.3120542422792,-30.6659673757733,13.0000000000021));
#4307=CARTESIAN_POINT('Ctrl Pts',(-29.3120542422792,-30.0000000000105,13.0000000000021));
#4308=CARTESIAN_POINT('Ctrl Pts',(-29.3120542422792,-30.0000000000105,13.0000000000021));
#4309=CARTESIAN_POINT('Ctrl Pts',(-29.3120542422792,-29.3340326242477,13.0000000000021));
#4310=CARTESIAN_POINT('Ctrl Pts',(-29.4527956614068,-28.6467782612167,12.8812351576426));
#4311=CARTESIAN_POINT('Ctrl Pts',(-29.9764667659311,-27.4219616375112,12.4565421384626));
#4312=CARTESIAN_POINT('Ctrl Pts',(-30.3579885926001,-26.8829978378241,12.1529255036342));
#4313=CARTESIAN_POINT('Ctrl Pts',(-31.2127810222979,-26.0282054081263,11.5295040511826));
#4314=CARTESIAN_POINT('Ctrl Pts',(-31.7522928141166,-25.6555960486084,11.1575129861594));
#4315=CARTESIAN_POINT('Ctrl Pts',(-32.6532784827973,-25.2718905240171,10.6992796672134));
#4316=CARTESIAN_POINT('Ctrl Pts',(-32.9692326416159,-25.172067656002,10.564392312562));
#4317=CARTESIAN_POINT('Ctrl Pts',(-33.6249191325797,-25.0361359943163,10.372517968392));
#4318=CARTESIAN_POINT('Ctrl Pts',(-33.9649654150723,-25.0000000000105,10.3166247903575));
#4319=CARTESIAN_POINT('Ctrl Pts',(-34.6591430694861,-25.0000000000105,10.3166247903575));
#4320=CARTESIAN_POINT('Ctrl Pts',(-34.9991893519787,-25.0361359943163,10.372517968392));
#4321=CARTESIAN_POINT('Ctrl Pts',(-35.6548758429425,-25.172067656002,10.564392312562));
#4322=CARTESIAN_POINT('Ctrl Pts',(-35.9708300017611,-25.2718905240171,10.6992796672134));
#4323=CARTESIAN_POINT('Ctrl Pts',(-36.8718156704418,-25.6555960486084,11.1575129861594));
#4324=CARTESIAN_POINT('Ctrl Pts',(-37.4113274622605,-26.0282054081263,11.5295040511826));
#4325=CARTESIAN_POINT('Ctrl Pts',(-38.2661198919583,-26.8829978378241,12.1529255036342));
#4326=CARTESIAN_POINT('Ctrl Pts',(-38.6476417186273,-27.4219616375112,12.4565421384626));
#4327=CARTESIAN_POINT('Ctrl Pts',(-39.1713128231516,-28.6467782612166,12.8812351576426));
#4328=CARTESIAN_POINT('Ctrl Pts',(-39.3120542422792,-29.3340326242477,13.0000000000021));
#4329=CARTESIAN_POINT('Ctrl Pts',(-39.3120542422792,-30.6659673757733,13.0000000000021));
#4330=CARTESIAN_POINT('Ctrl Pts',(-39.1713128231516,-31.3532217388044,12.8812351576426));
#4331=CARTESIAN_POINT('Ctrl Pts',(-38.6476417186273,-32.5780383625099,12.4565421384626));
#4332=CARTESIAN_POINT('Ctrl Pts',(-38.2661198919583,-33.1170021621969,12.1529255036342));
#4333=CARTESIAN_POINT('Ctrl Pts',(-37.4113274622605,-33.9717945918947,11.5295040511826));
#4334=CARTESIAN_POINT('Ctrl Pts',(-36.8718156704418,-34.3444039514126,11.1575129861594));
#4335=CARTESIAN_POINT('Ctrl Pts',(-35.9708300017611,-34.7281094760039,10.6992796672134));
#4336=CARTESIAN_POINT('Ctrl Pts',(-35.6548758429425,-34.8279323440191,10.564392312562));
#4337=CARTESIAN_POINT('Ctrl Pts',(-34.9991893519787,-34.9638640057048,10.372517968392));
#4338=CARTESIAN_POINT('Ctrl Pts',(-34.6591430694861,-35.0000000000105,10.3166247903575));
#4339=CARTESIAN_POINT('Ctrl Pts',(-34.3120542422792,-35.0000000000105,10.3166247903575));
#4340=CARTESIAN_POINT('Origin',(-34.3120542422792,-30.0000000000105,20.0000000000021));
#4341=CARTESIAN_POINT('',(-34.3120542422792,-35.0000000000105,3.68337520964672));
#4342=CARTESIAN_POINT('',(-29.3120542422792,-30.0000000000105,1.00000000000212));
#4343=CARTESIAN_POINT('Ctrl Pts',(-34.3120542422792,-35.0000000000105,3.68337520964672));
#4344=CARTESIAN_POINT('Ctrl Pts',(-34.6591430694861,-35.0000000000105,3.68337520964672));
#4345=CARTESIAN_POINT('Ctrl Pts',(-34.9991893519787,-34.9638640057048,3.62748203161225));
#4346=CARTESIAN_POINT('Ctrl Pts',(-35.6548758429425,-34.8279323440191,3.43560768744221));
#4347=CARTESIAN_POINT('Ctrl Pts',(-35.9708300017611,-34.7281094760039,3.30072033279082));
#4348=CARTESIAN_POINT('Ctrl Pts',(-36.8718156704418,-34.3444039514126,2.84248701384487));
#4349=CARTESIAN_POINT('Ctrl Pts',(-37.4113274622605,-33.9717945918947,2.47049594882166));
#4350=CARTESIAN_POINT('Ctrl Pts',(-38.2661198919583,-33.1170021621969,1.84707449637));
#4351=CARTESIAN_POINT('Ctrl Pts',(-38.6476417186273,-32.5780383625099,1.54345786154165));
#4352=CARTESIAN_POINT('Ctrl Pts',(-39.1713128231516,-31.3532217388044,1.1187648423616));
#4353=CARTESIAN_POINT('Ctrl Pts',(-39.3120542422792,-30.6659673757733,1.00000000000212));
#4354=CARTESIAN_POINT('Ctrl Pts',(-39.3120542422792,-29.3340326242477,1.00000000000212));
#4355=CARTESIAN_POINT('Ctrl Pts',(-39.1713128231516,-28.6467782612166,1.1187648423616));
#4356=CARTESIAN_POINT('Ctrl Pts',(-38.6476417186273,-27.4219616375112,1.54345786154166));
#4357=CARTESIAN_POINT('Ctrl Pts',(-38.2661198919583,-26.8829978378241,1.84707449637));
#4358=CARTESIAN_POINT('Ctrl Pts',(-37.4113274622605,-26.0282054081263,2.47049594882166));
#4359=CARTESIAN_POINT('Ctrl Pts',(-36.8718156704418,-25.6555960486084,2.84248701384487));
#4360=CARTESIAN_POINT('Ctrl Pts',(-35.9708300017611,-25.2718905240171,3.30072033279082));
#4361=CARTESIAN_POINT('Ctrl Pts',(-35.6548758429425,-25.172067656002,3.43560768744221));
#4362=CARTESIAN_POINT('Ctrl Pts',(-34.9991893519787,-25.0361359943163,3.62748203161225));
#4363=CARTESIAN_POINT('Ctrl Pts',(-34.6591430694861,-25.0000000000105,3.68337520964672));
#4364=CARTESIAN_POINT('Ctrl Pts',(-33.9649654150723,-25.0000000000105,3.68337520964672));
#4365=CARTESIAN_POINT('Ctrl Pts',(-33.6249191325797,-25.0361359943163,3.62748203161224));
#4366=CARTESIAN_POINT('Ctrl Pts',(-32.9692326416159,-25.172067656002,3.43560768744219));
#4367=CARTESIAN_POINT('Ctrl Pts',(-32.6532784827973,-25.2718905240171,3.30072033279081));
#4368=CARTESIAN_POINT('Ctrl Pts',(-31.7522928141166,-25.6555960486084,2.84248701384486));
#4369=CARTESIAN_POINT('Ctrl Pts',(-31.2127810222979,-26.0282054081263,2.47049594882166));
#4370=CARTESIAN_POINT('Ctrl Pts',(-30.3579885926001,-26.8829978378241,1.84707449636999));
#4371=CARTESIAN_POINT('Ctrl Pts',(-29.9764667659311,-27.4219616375112,1.54345786154165));
#4372=CARTESIAN_POINT('Ctrl Pts',(-29.4527956614068,-28.6467782612166,1.1187648423616));
#4373=CARTESIAN_POINT('Ctrl Pts',(-29.3120542422792,-29.3340326242477,1.00000000000212));
#4374=CARTESIAN_POINT('Ctrl Pts',(-29.3120542422792,-30.0000000000105,1.00000000000212));
#4375=CARTESIAN_POINT('Ctrl Pts',(-29.3120542422792,-30.0000000000105,1.00000000000212));
#4376=CARTESIAN_POINT('Ctrl Pts',(-29.3120542422792,-30.6659673757733,1.00000000000212));
#4377=CARTESIAN_POINT('Ctrl Pts',(-29.4527956614068,-31.3532217388044,1.1187648423616));
#4378=CARTESIAN_POINT('Ctrl Pts',(-29.9764667659311,-32.5780383625098,1.54345786154165));
#4379=CARTESIAN_POINT('Ctrl Pts',(-30.3579885926001,-33.1170021621969,1.84707449636999));
#4380=CARTESIAN_POINT('Ctrl Pts',(-31.2127810222979,-33.9717945918947,2.47049594882166));
#4381=CARTESIAN_POINT('Ctrl Pts',(-31.7522928141166,-34.3444039514126,2.84248701384486));
#4382=CARTESIAN_POINT('Ctrl Pts',(-32.6532784827973,-34.7281094760039,3.30072033279081));
#4383=CARTESIAN_POINT('Ctrl Pts',(-32.9692326416159,-34.8279323440191,3.43560768744219));
#4384=CARTESIAN_POINT('Ctrl Pts',(-33.6249191325797,-34.9638640057048,3.62748203161224));
#4385=CARTESIAN_POINT('Ctrl Pts',(-33.9649654150723,-35.0000000000105,3.68337520964672));
#4386=CARTESIAN_POINT('Ctrl Pts',(-34.3120542422792,-35.0000000000105,3.68337520964672));
#4387=CARTESIAN_POINT('',(-29.3120542422792,-30.0000000000105,-5.99999999999788));
#4388=CARTESIAN_POINT('',(-29.3120542422792,-30.0000000000105,20.0000000000021));
#4389=CARTESIAN_POINT('Origin',(-34.3120542422792,-30.0000000000105,-5.99999999999788));
#4390=CARTESIAN_POINT('Origin',(-34.3120542422792,14.9999999999895,20.0000000000021));
#4391=CARTESIAN_POINT('',(-29.3120542422792,14.9999999999895,20.0000000000021));
#4392=CARTESIAN_POINT('Origin',(-34.3120542422792,14.9999999999895,20.0000000000021));
#4393=CARTESIAN_POINT('',(-29.3120542422792,14.9999999999895,14.0000000000021));
#4394=CARTESIAN_POINT('',(-29.3120542422792,14.9999999999895,20.0000000000021));
#4395=CARTESIAN_POINT('Origin',(-34.3120542422792,14.9999999999895,14.0000000000021));
#4396=CARTESIAN_POINT('Origin',(-14.3120542422792,-75.0000000000105,20.0000000000021));
#4397=CARTESIAN_POINT('',(-9.3120542422792,-75.0000000000105,20.0000000000021));
#4398=CARTESIAN_POINT('Origin',(-14.3120542422792,-75.0000000000105,20.0000000000021));
#4399=CARTESIAN_POINT('',(-9.3120542422792,-75.0000000000105,14.0000000000021));
#4400=CARTESIAN_POINT('',(-9.3120542422792,-75.0000000000105,20.0000000000021));
#4401=CARTESIAN_POINT('Origin',(-14.3120542422792,-75.0000000000105,14.0000000000021));
#4402=CARTESIAN_POINT('Origin',(10.6879457577208,-30.0000000000105,20.0000000000021));
#4403=CARTESIAN_POINT('',(15.6879457577208,-30.0000000000105,20.0000000000021));
#4404=CARTESIAN_POINT('Origin',(10.6879457577208,-30.0000000000105,20.0000000000021));
#4405=CARTESIAN_POINT('',(15.6879457577208,-30.0000000000105,13.0000000000021));
#4406=CARTESIAN_POINT('',(15.6879457577208,-30.0000000000105,20.0000000000021));
#4407=CARTESIAN_POINT('',(10.6879457577208,-35.0000000000105,10.3166247903575));
#4408=CARTESIAN_POINT('Ctrl Pts',(10.6879457577208,-35.0000000000105,10.3166247903575));
#4409=CARTESIAN_POINT('Ctrl Pts',(11.0350345849277,-35.0000000000105,10.3166247903575));
#4410=CARTESIAN_POINT('Ctrl Pts',(11.3750808674203,-34.9638640057048,10.372517968392));
#4411=CARTESIAN_POINT('Ctrl Pts',(12.0307673583841,-34.8279323440191,10.564392312562));
#4412=CARTESIAN_POINT('Ctrl Pts',(12.3467215172027,-34.7281094760039,10.6992796672134));
#4413=CARTESIAN_POINT('Ctrl Pts',(13.2477071858834,-34.3444039514126,11.1575129861594));
#4414=CARTESIAN_POINT('Ctrl Pts',(13.7872189777021,-33.9717945918947,11.5295040511826));
#4415=CARTESIAN_POINT('Ctrl Pts',(14.6420114073999,-33.1170021621969,12.1529255036342));
#4416=CARTESIAN_POINT('Ctrl Pts',(15.0235332340689,-32.5780383625099,12.4565421384626));
#4417=CARTESIAN_POINT('Ctrl Pts',(15.5472043385932,-31.3532217388044,12.8812351576426));
#4418=CARTESIAN_POINT('Ctrl Pts',(15.6879457577208,-30.6659673757733,13.0000000000021));
#4419=CARTESIAN_POINT('Ctrl Pts',(15.6879457577208,-30.0000000000105,13.0000000000021));
#4420=CARTESIAN_POINT('Ctrl Pts',(15.6879457577208,-30.0000000000105,13.0000000000021));
#4421=CARTESIAN_POINT('Ctrl Pts',(15.6879457577208,-29.3340326242477,13.0000000000021));
#4422=CARTESIAN_POINT('Ctrl Pts',(15.5472043385932,-28.6467782612166,12.8812351576426));
#4423=CARTESIAN_POINT('Ctrl Pts',(15.0235332340689,-27.4219616375112,12.4565421384626));
#4424=CARTESIAN_POINT('Ctrl Pts',(14.6420114073999,-26.8829978378241,12.1529255036342));
#4425=CARTESIAN_POINT('Ctrl Pts',(13.7872189777021,-26.0282054081263,11.5295040511826));
#4426=CARTESIAN_POINT('Ctrl Pts',(13.2477071858834,-25.6555960486084,11.1575129861594));
#4427=CARTESIAN_POINT('Ctrl Pts',(12.3467215172027,-25.2718905240171,10.6992796672134));
#4428=CARTESIAN_POINT('Ctrl Pts',(12.0307673583841,-25.172067656002,10.564392312562));
#4429=CARTESIAN_POINT('Ctrl Pts',(11.3750808674203,-25.0361359943163,10.372517968392));
#4430=CARTESIAN_POINT('Ctrl Pts',(11.0350345849277,-25.0000000000105,10.3166247903575));
#4431=CARTESIAN_POINT('Ctrl Pts',(10.3408569305139,-25.0000000000105,10.3166247903575));
#4432=CARTESIAN_POINT('Ctrl Pts',(10.0008106480213,-25.0361359943163,10.372517968392));
#4433=CARTESIAN_POINT('Ctrl Pts',(9.3451241570575,-25.172067656002,10.564392312562));
#4434=CARTESIAN_POINT('Ctrl Pts',(9.02916999823889,-25.2718905240171,10.6992796672134));
#4435=CARTESIAN_POINT('Ctrl Pts',(8.12818432955822,-25.6555960486084,11.1575129861594));
#4436=CARTESIAN_POINT('Ctrl Pts',(7.58867253773952,-26.0282054081263,11.5295040511826));
#4437=CARTESIAN_POINT('Ctrl Pts',(6.73388010804173,-26.8829978378241,12.1529255036342));
#4438=CARTESIAN_POINT('Ctrl Pts',(6.3523582813727,-27.4219616375112,12.4565421384626));
#4439=CARTESIAN_POINT('Ctrl Pts',(5.8286871768484,-28.6467782612166,12.8812351576426));
#4440=CARTESIAN_POINT('Ctrl Pts',(5.6879457577208,-29.3340326242477,13.0000000000021));
#4441=CARTESIAN_POINT('Ctrl Pts',(5.6879457577208,-30.6659673757733,13.0000000000021));
#4442=CARTESIAN_POINT('Ctrl Pts',(5.8286871768484,-31.3532217388044,12.8812351576426));
#4443=CARTESIAN_POINT('Ctrl Pts',(6.3523582813727,-32.5780383625099,12.4565421384626));
#4444=CARTESIAN_POINT('Ctrl Pts',(6.73388010804173,-33.1170021621969,12.1529255036342));
#4445=CARTESIAN_POINT('Ctrl Pts',(7.58867253773952,-33.9717945918947,11.5295040511826));
#4446=CARTESIAN_POINT('Ctrl Pts',(8.12818432955822,-34.3444039514126,11.1575129861594));
#4447=CARTESIAN_POINT('Ctrl Pts',(9.0291699982389,-34.7281094760039,10.6992796672134));
#4448=CARTESIAN_POINT('Ctrl Pts',(9.34512415705749,-34.8279323440191,10.564392312562));
#4449=CARTESIAN_POINT('Ctrl Pts',(10.0008106480213,-34.9638640057048,10.372517968392));
#4450=CARTESIAN_POINT('Ctrl Pts',(10.3408569305139,-35.0000000000105,10.3166247903575));
#4451=CARTESIAN_POINT('Ctrl Pts',(10.6879457577208,-35.0000000000105,10.3166247903575));
#4452=CARTESIAN_POINT('Origin',(10.6879457577208,-30.0000000000105,20.0000000000021));
#4453=CARTESIAN_POINT('',(10.6879457577208,-35.0000000000105,3.68337520964672));
#4454=CARTESIAN_POINT('',(15.6879457577208,-30.0000000000105,1.00000000000212));
#4455=CARTESIAN_POINT('Ctrl Pts',(10.6879457577208,-35.0000000000105,3.68337520964672));
#4456=CARTESIAN_POINT('Ctrl Pts',(10.3408569305139,-35.0000000000105,3.68337520964672));
#4457=CARTESIAN_POINT('Ctrl Pts',(10.0008106480213,-34.9638640057048,3.62748203161225));
#4458=CARTESIAN_POINT('Ctrl Pts',(9.3451241570575,-34.8279323440191,3.4356076874422));
#4459=CARTESIAN_POINT('Ctrl Pts',(9.02916999823889,-34.7281094760039,3.30072033279082));
#4460=CARTESIAN_POINT('Ctrl Pts',(8.12818432955822,-34.3444039514126,2.84248701384487));
#4461=CARTESIAN_POINT('Ctrl Pts',(7.58867253773952,-33.9717945918947,2.47049594882166));
#4462=CARTESIAN_POINT('Ctrl Pts',(6.73388010804173,-33.1170021621969,1.84707449637));
#4463=CARTESIAN_POINT('Ctrl Pts',(6.3523582813727,-32.5780383625099,1.54345786154165));
#4464=CARTESIAN_POINT('Ctrl Pts',(5.8286871768484,-31.3532217388044,1.1187648423616));
#4465=CARTESIAN_POINT('Ctrl Pts',(5.6879457577208,-30.6659673757733,1.00000000000212));
#4466=CARTESIAN_POINT('Ctrl Pts',(5.6879457577208,-29.3340326242477,1.00000000000212));
#4467=CARTESIAN_POINT('Ctrl Pts',(5.8286871768484,-28.6467782612166,1.1187648423616));
#4468=CARTESIAN_POINT('Ctrl Pts',(6.3523582813727,-27.4219616375112,1.54345786154165));
#4469=CARTESIAN_POINT('Ctrl Pts',(6.73388010804173,-26.8829978378241,1.84707449637));
#4470=CARTESIAN_POINT('Ctrl Pts',(7.58867253773952,-26.0282054081263,2.47049594882166));
#4471=CARTESIAN_POINT('Ctrl Pts',(8.12818432955822,-25.6555960486084,2.84248701384487));
#4472=CARTESIAN_POINT('Ctrl Pts',(9.02916999823889,-25.2718905240171,3.30072033279082));
#4473=CARTESIAN_POINT('Ctrl Pts',(9.3451241570575,-25.172067656002,3.4356076874422));
#4474=CARTESIAN_POINT('Ctrl Pts',(10.0008106480213,-25.0361359943163,3.62748203161225));
#4475=CARTESIAN_POINT('Ctrl Pts',(10.3408569305139,-25.0000000000105,3.68337520964672));
#4476=CARTESIAN_POINT('Ctrl Pts',(11.0350345849277,-25.0000000000105,3.68337520964672));
#4477=CARTESIAN_POINT('Ctrl Pts',(11.3750808674203,-25.0361359943163,3.62748203161225));
#4478=CARTESIAN_POINT('Ctrl Pts',(12.0307673583841,-25.172067656002,3.43560768744221));
#4479=CARTESIAN_POINT('Ctrl Pts',(12.3467215172027,-25.2718905240171,3.30072033279082));
#4480=CARTESIAN_POINT('Ctrl Pts',(13.2477071858834,-25.6555960486084,2.84248701384486));
#4481=CARTESIAN_POINT('Ctrl Pts',(13.7872189777021,-26.0282054081263,2.47049594882166));
#4482=CARTESIAN_POINT('Ctrl Pts',(14.6420114073999,-26.8829978378241,1.84707449637));
#4483=CARTESIAN_POINT('Ctrl Pts',(15.0235332340689,-27.4219616375112,1.54345786154165));
#4484=CARTESIAN_POINT('Ctrl Pts',(15.5472043385932,-28.6467782612166,1.1187648423616));
#4485=CARTESIAN_POINT('Ctrl Pts',(15.6879457577208,-29.3340326242477,1.00000000000212));
#4486=CARTESIAN_POINT('Ctrl Pts',(15.6879457577208,-30.0000000000105,1.00000000000212));
#4487=CARTESIAN_POINT('Ctrl Pts',(15.6879457577208,-30.0000000000105,1.00000000000212));
#4488=CARTESIAN_POINT('Ctrl Pts',(15.6879457577208,-30.6659673757733,1.00000000000212));
#4489=CARTESIAN_POINT('Ctrl Pts',(15.5472043385932,-31.3532217388044,1.1187648423616));
#4490=CARTESIAN_POINT('Ctrl Pts',(15.0235332340689,-32.5780383625098,1.54345786154165));
#4491=CARTESIAN_POINT('Ctrl Pts',(14.6420114073999,-33.1170021621969,1.84707449637));
#4492=CARTESIAN_POINT('Ctrl Pts',(13.7872189777021,-33.9717945918947,2.47049594882166));
#4493=CARTESIAN_POINT('Ctrl Pts',(13.2477071858834,-34.3444039514126,2.84248701384487));
#4494=CARTESIAN_POINT('Ctrl Pts',(12.3467215172027,-34.7281094760039,3.30072033279082));
#4495=CARTESIAN_POINT('Ctrl Pts',(12.0307673583841,-34.8279323440191,3.43560768744221));
#4496=CARTESIAN_POINT('Ctrl Pts',(11.3750808674203,-34.9638640057048,3.62748203161225));
#4497=CARTESIAN_POINT('Ctrl Pts',(11.0350345849277,-35.0000000000105,3.68337520964672));
#4498=CARTESIAN_POINT('Ctrl Pts',(10.6879457577208,-35.0000000000105,3.68337520964672));
#4499=CARTESIAN_POINT('',(15.6879457577208,-30.0000000000105,-5.99999999999788));
#4500=CARTESIAN_POINT('',(15.6879457577208,-30.0000000000105,20.0000000000021));
#4501=CARTESIAN_POINT('Origin',(10.6879457577208,-30.0000000000105,-5.99999999999788));
#4502=CARTESIAN_POINT('Origin',(-9.3120542422792,14.9999999999895,20.0000000000021));
#4503=CARTESIAN_POINT('',(-4.3120542422792,14.9999999999895,20.0000000000021));
#4504=CARTESIAN_POINT('Origin',(-9.3120542422792,14.9999999999895,20.0000000000021));
#4505=CARTESIAN_POINT('',(-4.3120542422792,14.9999999999895,14.0000000000021));
#4506=CARTESIAN_POINT('',(-4.3120542422792,14.9999999999895,20.0000000000021));
#4507=CARTESIAN_POINT('Origin',(-9.3120542422792,14.9999999999895,14.0000000000021));
#4508=CARTESIAN_POINT('Origin',(10.6879457577208,-75.0000000000105,20.0000000000021));
#4509=CARTESIAN_POINT('',(15.6879457577208,-75.0000000000105,20.0000000000021));
#4510=CARTESIAN_POINT('Origin',(10.6879457577208,-75.0000000000105,20.0000000000021));
#4511=CARTESIAN_POINT('',(15.6879457577208,-75.0000000000105,14.0000000000021));
#4512=CARTESIAN_POINT('',(15.6879457577208,-75.0000000000105,20.0000000000021));
#4513=CARTESIAN_POINT('Origin',(10.6879457577208,-75.0000000000105,14.0000000000021));
#4514=CARTESIAN_POINT('Origin',(29.,28.9999999999895,19.0000000000021));
#4515=CARTESIAN_POINT('',(30.,28.9999999999895,19.0000000000021));
#4516=CARTESIAN_POINT('',(29.,28.9999999999895,20.0000000000021));
#4517=CARTESIAN_POINT('Origin',(29.,28.9999999999895,19.0000000000021));
#4518=CARTESIAN_POINT('',(29.,29.9999999999895,19.0000000000021));
#4519=CARTESIAN_POINT('Origin',(29.,28.9999999999895,19.0000000000021));
#4520=CARTESIAN_POINT('Origin',(29.,28.9999999999895,19.0000000000021));
#4521=CARTESIAN_POINT('Origin',(29.,28.9999999999895,-5.99999999999788));
#4522=CARTESIAN_POINT('',(30.,28.9999999999895,4.00000000000212));
#4523=CARTESIAN_POINT('',(29.,29.9999999999895,4.00000000000212));
#4524=CARTESIAN_POINT('Origin',(29.,28.9999999999895,4.00000000000212));
#4525=CARTESIAN_POINT('',(29.,29.9999999999895,-5.99999999999788));
#4526=CARTESIAN_POINT('',(30.,28.9999999999895,-5.99999999999788));
#4527=CARTESIAN_POINT('Origin',(-49.,28.9999999999895,19.0000000000021));
#4528=CARTESIAN_POINT('',(-49.,29.9999999999895,19.0000000000021));
#4529=CARTESIAN_POINT('',(-49.,28.9999999999895,20.0000000000021));
#4530=CARTESIAN_POINT('Origin',(-49.,28.9999999999895,19.0000000000021));
#4531=CARTESIAN_POINT('',(-50.,28.9999999999895,19.0000000000021));
#4532=CARTESIAN_POINT('Origin',(-49.,28.9999999999895,19.0000000000021));
#4533=CARTESIAN_POINT('Origin',(-49.,28.9999999999895,19.0000000000021));
#4534=CARTESIAN_POINT('Origin',(-49.,28.9999999999895,-5.99999999999788));
#4535=CARTESIAN_POINT('',(-49.,29.9999999999895,4.00000000000212));
#4536=CARTESIAN_POINT('',(-50.,28.9999999999895,4.00000000000212));
#4537=CARTESIAN_POINT('Origin',(-49.,28.9999999999895,4.00000000000212));
#4538=CARTESIAN_POINT('',(-50.,28.9999999999895,-5.99999999999788));
#4539=CARTESIAN_POINT('',(-49.,29.9999999999895,-5.99999999999788));
#4540=CARTESIAN_POINT('Origin',(29.,-89.0000000000105,19.0000000000021));
#4541=CARTESIAN_POINT('',(29.,-90.0000000000105,19.0000000000021));
#4542=CARTESIAN_POINT('',(29.,-89.0000000000105,20.0000000000021));
#4543=CARTESIAN_POINT('Origin',(29.,-89.0000000000105,19.0000000000021));
#4544=CARTESIAN_POINT('',(30.,-89.0000000000105,19.0000000000021));
#4545=CARTESIAN_POINT('Origin',(29.,-89.0000000000105,19.0000000000021));
#4546=CARTESIAN_POINT('Origin',(29.,-89.0000000000105,19.0000000000021));
#4547=CARTESIAN_POINT('Origin',(29.,-89.0000000000105,-5.99999999999788));
#4548=CARTESIAN_POINT('',(29.,-90.0000000000105,4.00000000000212));
#4549=CARTESIAN_POINT('',(30.,-89.0000000000105,4.00000000000212));
#4550=CARTESIAN_POINT('Origin',(29.,-89.0000000000105,4.00000000000212));
#4551=CARTESIAN_POINT('',(30.,-89.0000000000105,-5.99999999999788));
#4552=CARTESIAN_POINT('',(29.,-90.0000000000105,-5.99999999999788));
#4553=CARTESIAN_POINT('Origin',(29.,-60.0000000000105,19.0000000000021));
#4554=CARTESIAN_POINT('',(29.,-60.0000000000105,20.0000000000021));
#4555=CARTESIAN_POINT('',(30.,-60.0000000000105,19.0000000000021));
#4556=CARTESIAN_POINT('Origin',(-49.,-89.0000000000105,19.0000000000021));
#4557=CARTESIAN_POINT('',(-50.,-89.0000000000105,19.0000000000021));
#4558=CARTESIAN_POINT('',(-49.,-89.0000000000105,20.0000000000021));
#4559=CARTESIAN_POINT('Origin',(-49.,-89.0000000000105,19.0000000000021));
#4560=CARTESIAN_POINT('',(-49.,-90.0000000000105,19.0000000000021));
#4561=CARTESIAN_POINT('Origin',(-49.,-89.0000000000105,19.0000000000021));
#4562=CARTESIAN_POINT('Origin',(-49.,-89.0000000000105,19.0000000000021));
#4563=CARTESIAN_POINT('Origin',(-49.,-89.0000000000105,-5.99999999999788));
#4564=CARTESIAN_POINT('',(-50.,-89.0000000000105,4.00000000000212));
#4565=CARTESIAN_POINT('',(-49.,-90.0000000000105,4.00000000000212));
#4566=CARTESIAN_POINT('Origin',(-49.,-89.0000000000105,4.00000000000212));
#4567=CARTESIAN_POINT('',(-49.,-90.0000000000105,-5.99999999999788));
#4568=CARTESIAN_POINT('',(-50.,-89.0000000000105,-5.99999999999788));
#4569=CARTESIAN_POINT('Origin',(-30.,-89.0000000000105,19.0000000000021));
#4570=CARTESIAN_POINT('',(-30.,-89.0000000000105,20.0000000000021));
#4571=CARTESIAN_POINT('',(-30.,-90.0000000000105,19.0000000000021));
#4572=CARTESIAN_POINT('Origin',(-49.,-1.05160324892495E-11,19.0000000000021));
#4573=CARTESIAN_POINT('',(-49.,-1.05160324892495E-11,20.0000000000021));
#4574=CARTESIAN_POINT('',(-50.,-1.05160324892495E-11,19.0000000000021));
#4575=CARTESIAN_POINT('Origin',(10.,28.9999999999895,19.0000000000021));
#4576=CARTESIAN_POINT('',(10.,28.9999999999895,20.0000000000021));
#4577=CARTESIAN_POINT('',(10.,29.9999999999895,19.0000000000021));
#4578=CARTESIAN_POINT('Origin',(30.,-90.0000000000105,-5.99999999999788));
#4579=CARTESIAN_POINT('',(30.,-81.0000000000105,4.00000000000212));
#4580=CARTESIAN_POINT('',(30.,-82.5000000000105,4.00000000000212));
#4581=CARTESIAN_POINT('',(30.,-81.0000000000105,14.0000000000021));
#4582=CARTESIAN_POINT('',(30.,-81.0000000000105,-0.999999999997885));
#4583=CARTESIAN_POINT('',(30.,-69.0000000000105,14.0000000000021));
#4584=CARTESIAN_POINT('',(30.,-82.5000000000105,14.0000000000021));
#4585=CARTESIAN_POINT('',(30.,-69.0000000000105,4.00000000000212));
#4586=CARTESIAN_POINT('',(30.,-69.0000000000105,-0.999999999997885));
#4587=CARTESIAN_POINT('',(30.,-60.0000000000105,4.00000000000212));
#4588=CARTESIAN_POINT('',(30.,-82.5000000000105,4.00000000000212));
#4589=CARTESIAN_POINT('',(30.,-60.0000000000105,-5.99999999999788));
#4590=CARTESIAN_POINT('',(30.,-60.0000000000105,-5.99999999999788));
#4591=CARTESIAN_POINT('',(30.,-1.05160324892495E-11,-5.99999999999788));
#4592=CARTESIAN_POINT('',(30.,29.9999999999895,-5.99999999999788));
#4593=CARTESIAN_POINT('',(30.,-1.05160324892495E-11,4.00000000000212));
#4594=CARTESIAN_POINT('',(30.,-1.05160324892495E-11,-5.99999999999788));
#4595=CARTESIAN_POINT('',(30.,8.99999999998949,4.00000000000212));
#4596=CARTESIAN_POINT('',(30.,-37.5000000000105,4.00000000000212));
#4597=CARTESIAN_POINT('',(30.,8.99999999998948,14.0000000000021));
#4598=CARTESIAN_POINT('',(30.,8.99999999998949,-0.999999999997885));
#4599=CARTESIAN_POINT('',(30.,20.9999999999895,14.0000000000021));
#4600=CARTESIAN_POINT('',(30.,-37.5000000000105,14.0000000000021));
#4601=CARTESIAN_POINT('',(30.,20.9999999999895,4.00000000000212));
#4602=CARTESIAN_POINT('',(30.,20.9999999999895,-0.999999999997885));
#4603=CARTESIAN_POINT('',(30.,-37.5000000000105,4.00000000000212));
#4604=CARTESIAN_POINT('',(30.,-24.0000000000105,7.00000000000211));
#4605=CARTESIAN_POINT('Origin',(30.,-30.0000000000105,7.00000000000211));
#4606=CARTESIAN_POINT('Origin',(-50.,-90.0000000000105,-5.99999999999788));
#4607=CARTESIAN_POINT('',(-30.,-90.0000000000105,4.00000000000212));
#4608=CARTESIAN_POINT('Origin',(-10.,-75.0000000000105,4.00000000000212));
#4609=CARTESIAN_POINT('',(-50.,-81.0000000000105,4.00000000000212));
#4610=CARTESIAN_POINT('',(-50.,-22.5000000000105,4.00000000000212));
#4611=CARTESIAN_POINT('',(-50.,-81.0000000000105,4.00000000000212));
#4612=CARTESIAN_POINT('Origin',(-10.,-30.0000000000105,20.0000000000021));
#4613=CARTESIAN_POINT('Origin',(70.,-30.0000000000105,7.00000000000211));
#4614=CARTESIAN_POINT('',(-50.,-24.0000000000105,7.00000000000211));
#4615=CARTESIAN_POINT('',(70.,-24.0000000000105,7.00000000000211));
#4616=CARTESIAN_POINT('Origin',(-50.,-30.0000000000105,7.00000000000211));
#4617=CARTESIAN_POINT('Origin',(-90.,8.99999999998948,4.00000000000212));
#4618=CARTESIAN_POINT('',(-50.,8.99999999998948,14.0000000000021));
#4619=CARTESIAN_POINT('',(-50.,8.99999999998948,4.00000000000212));
#4620=CARTESIAN_POINT('',(-50.,8.99999999998948,-0.999999999997885));
#4621=CARTESIAN_POINT('',(70.,8.99999999998948,14.0000000000021));
#4622=CARTESIAN_POINT('',(-50.,8.99999999998948,4.00000000000212));
#4623=CARTESIAN_POINT('Origin',(70.,20.9999999999895,4.00000000000212));
#4624=CARTESIAN_POINT('',(-50.,20.9999999999895,4.00000000000212));
#4625=CARTESIAN_POINT('',(-50.,20.9999999999895,14.0000000000021));
#4626=CARTESIAN_POINT('',(-50.,20.9999999999895,-0.999999999997885));
#4627=CARTESIAN_POINT('',(30.,20.9999999999895,4.00000000000212));
#4628=CARTESIAN_POINT('',(-90.,20.9999999999895,14.0000000000021));
#4629=CARTESIAN_POINT('Origin',(-10.,14.9999999999895,14.0000000000021));
#4630=CARTESIAN_POINT('',(-50.,22.4999999999895,14.0000000000021));
#4631=CARTESIAN_POINT('Origin',(-90.,-81.0000000000105,4.00000000000212));
#4632=CARTESIAN_POINT('',(-50.,-81.0000000000105,14.0000000000021));
#4633=CARTESIAN_POINT('',(-50.,-81.0000000000105,-0.999999999997885));
#4634=CARTESIAN_POINT('',(-90.,-81.0000000000105,14.0000000000021));
#4635=CARTESIAN_POINT('Origin',(70.,-69.0000000000105,4.00000000000212));
#4636=CARTESIAN_POINT('',(-50.,-69.0000000000105,4.00000000000212));
#4637=CARTESIAN_POINT('',(-50.,-69.0000000000105,14.0000000000021));
#4638=CARTESIAN_POINT('',(-50.,-69.0000000000105,-0.999999999997885));
#4639=CARTESIAN_POINT('',(30.,-69.0000000000105,4.00000000000212));
#4640=CARTESIAN_POINT('',(70.,-69.0000000000105,14.0000000000021));
#4641=CARTESIAN_POINT('Origin',(-10.,-75.0000000000105,14.0000000000021));
#4642=CARTESIAN_POINT('',(-50.,-22.5000000000105,14.0000000000021));
#4643=CARTESIAN_POINT('Origin',(-10.,14.9999999999895,4.00000000000212));
#4644=CARTESIAN_POINT('',(-50.,22.4999999999895,4.00000000000212));
#4645=CARTESIAN_POINT('',(10.,29.9999999999895,4.00000000000212));
#4646=CARTESIAN_POINT('Origin',(-10.,-75.0000000000105,4.00000000000212));
#4647=CARTESIAN_POINT('',(-50.,-60.0000000000105,4.00000000000212));
#4648=CARTESIAN_POINT('',(-50.,-22.5000000000105,4.00000000000212));
#4649=CARTESIAN_POINT('',(70.,-60.0000000000105,4.00000000000212));
#4650=CARTESIAN_POINT('Origin',(-10.,14.9999999999895,4.00000000000212));
#4651=CARTESIAN_POINT('',(-50.,-1.05160324892495E-11,4.00000000000212));
#4652=CARTESIAN_POINT('',(70.,-1.05160324892495E-11,4.00000000000212));
#4653=CARTESIAN_POINT('',(-50.,22.4999999999895,4.00000000000212));
#4654=CARTESIAN_POINT('Origin',(-90.,-1.05160324892495E-11,-5.99999999999788));
#4655=CARTESIAN_POINT('',(-50.,-1.05160324892495E-11,-5.99999999999788));
#4656=CARTESIAN_POINT('',(-50.,-1.05160324892495E-11,-5.99999999999788));
#4657=CARTESIAN_POINT('',(-50.,-1.05160324892495E-11,-5.99999999999788));
#4658=CARTESIAN_POINT('Origin',(70.,-60.0000000000105,-5.99999999999788));
#4659=CARTESIAN_POINT('',(-50.,-60.0000000000105,-5.99999999999788));
#4660=CARTESIAN_POINT('',(-50.,-60.0000000000105,-5.99999999999788));
#4661=CARTESIAN_POINT('',(30.,-60.0000000000105,-5.99999999999788));
#4662=CARTESIAN_POINT('Origin',(-50.,29.9999999999895,-5.99999999999788));
#4663=CARTESIAN_POINT('',(-50.,-90.0000000000105,-5.99999999999788));
#4664=CARTESIAN_POINT('Origin',(-10.,-30.0000000000105,-5.99999999999788));
#4665=CARTESIAN_POINT('Origin',(30.,29.9999999999895,-5.99999999999788));
#4816=UNCERTAINTY_MEASURE_WITH_UNIT(LENGTH_MEASURE(0.01),#4834,
'DISTANCE_ACCURACY_VALUE',
'Maximum model space distance between geometric entities at asserted c
onnectivities');
#4820=UNCERTAINTY_MEASURE_WITH_UNIT(LENGTH_MEASURE(0.01),#4834,
'DISTANCE_ACCURACY_VALUE',
'Maximum model space distance between geometric entities at asserted c
onnectivities');
#4829=(
GEOMETRIC_REPRESENTATION_CONTEXT(3)
GLOBAL_UNCERTAINTY_ASSIGNED_CONTEXT((#4816))
GLOBAL_UNIT_ASSIGNED_CONTEXT((#4834,#4836,#4837))
REPRESENTATION_CONTEXT('','3D')
);
#4833=(
GEOMETRIC_REPRESENTATION_CONTEXT(3)
GLOBAL_UNCERTAINTY_ASSIGNED_CONTEXT((#4820))
GLOBAL_UNIT_ASSIGNED_CONTEXT((#4834,#4836,#4837))
REPRESENTATION_CONTEXT('','3D')
);
#4834=(
LENGTH_UNIT()
NAMED_UNIT(*)
SI_UNIT(.MILLI.,.METRE.)
);
#4836=(
NAMED_UNIT(*)
PLANE_ANGLE_UNIT()
SI_UNIT($,.RADIAN.)
);
#4837=(
NAMED_UNIT(*)
SI_UNIT($,.STERADIAN.)
SOLID_ANGLE_UNIT()
);
#4846=SHAPE_DEFINITION_REPRESENTATION(#4858,#4881);
#4858=PRODUCT_DEFINITION_SHAPE('',$,#4894);
#4881=SHAPE_REPRESENTATION('',(#2970),#4829);
#4885=PRODUCT_DEFINITION_CONTEXT('part definition',#4923,'design');
#4894=PRODUCT_DEFINITION('Top_Block','Top_Block',#4906,#4885);
#4906=PRODUCT_DEFINITION_FORMATION('',$,#4933);
#4923=APPLICATION_CONTEXT(
'Core Data for Automotive Mechanical Design Process');
#4924=PRODUCT_CONTEXT('part definition',#4923,'mechanical');
#4933=PRODUCT('Top_Block','Top_Block',$,(#4924));
#4965=COLOUR_RGB('Dark Blue',0.08,0.2,0.34);
#4966=FILL_AREA_STYLE_COLOUR('',#4965);
#4967=FILL_AREA_STYLE('',(#4966));
#4968=SURFACE_STYLE_FILL_AREA(#4967);
#4969=SURFACE_SIDE_STYLE('',(#4968));
#4970=SURFACE_STYLE_USAGE(.BOTH.,#4969);
#4971=PRESENTATION_STYLE_ASSIGNMENT((#4970));
ENDSEC;
END-ISO-10303-21;
